ISO-10303-21;
HEADER;
/* Generated by software containing ST-Developer
 * from STEP Tools, Inc. (www.steptools.com) 
 */

FILE_DESCRIPTION(
/* description */ ('XY cross-slide table'),
/* implementation_level */ '2;1');

FILE_NAME(
/* name */ 'Flanged lead nut.step',
/* time_stamp */ '2026-10-28T03:22:46-07:00',
/* author */ (''),
/* organization */ (''),
/* preprocessor_version */ 'ST-DEVELOPER v20.2',
/* originating_system */ 'Autodesk Translation Framework v15.17.0.0',
/* authorisation */ '');

FILE_SCHEMA (('AUTOMOTIVE_DESIGN { 1 0 10303 214 3 1 1 }'));
ENDSEC;

DATA;
#10=MECHANICAL_DESIGN_GEOMETRIC_PRESENTATION_REPRESENTATION('',(#1714),#62984);
#11=B_SPLINE_SURFACE_WITH_KNOTS('',3,3,((#36306,#36307,#36308,#36309,#36310,
#36311,#36312,#36313,#36314,#36315,#36316,#36317,#36318,#36319,#36320,#36321,
#36322,#36323,#36324,#36325,#36326,#36327,#36328,#36329,#36330,#36331,#36332,
#36333,#36334,#36335,#36336,#36337,#36338,#36339,#36340,#36341,#36342,#36343,
#36344,#36345,#36346,#36347,#36348,#36349,#36350,#36351,#36352,#36353,#36354,
#36355,#36356,#36357,#36358,#36359,#36360,#36361,#36362,#36363,#36364,#36365,
#36366,#36367,#36368,#36369,#36370,#36371,#36372,#36373,#36374,#36375,#36376,
#36377,#36378,#36379,#36380,#36381,#36382,#36383,#36384,#36385,#36386,#36387,
#36388,#36389,#36390,#36391,#36392,#36393,#36394,#36395,#36396,#36397,#36398,
#36399,#36400,#36401,#36402,#36403,#36404,#36405,#36406,#36407,#36408,#36409,
#36410,#36411,#36412,#36413,#36414,#36415,#36416,#36417,#36418,#36419,#36420),
(#36421,#36422,#36423,#36424,#36425,#36426,#36427,#36428,#36429,#36430,
#36431,#36432,#36433,#36434,#36435,#36436,#36437,#36438,#36439,#36440,#36441,
#36442,#36443,#36444,#36445,#36446,#36447,#36448,#36449,#36450,#36451,#36452,
#36453,#36454,#36455,#36456,#36457,#36458,#36459,#36460,#36461,#36462,#36463,
#36464,#36465,#36466,#36467,#36468,#36469,#36470,#36471,#36472,#36473,#36474,
#36475,#36476,#36477,#36478,#36479,#36480,#36481,#36482,#36483,#36484,#36485,
#36486,#36487,#36488,#36489,#36490,#36491,#36492,#36493,#36494,#36495,#36496,
#36497,#36498,#36499,#36500,#36501,#36502,#36503,#36504,#36505,#36506,#36507,
#36508,#36509,#36510,#36511,#36512,#36513,#36514,#36515,#36516,#36517,#36518,
#36519,#36520,#36521,#36522,#36523,#36524,#36525,#36526,#36527,#36528,#36529,
#36530,#36531,#36532,#36533,#36534,#36535),(#36536,#36537,#36538,#36539,
#36540,#36541,#36542,#36543,#36544,#36545,#36546,#36547,#36548,#36549,#36550,
#36551,#36552,#36553,#36554,#36555,#36556,#36557,#36558,#36559,#36560,#36561,
#36562,#36563,#36564,#36565,#36566,#36567,#36568,#36569,#36570,#36571,#36572,
#36573,#36574,#36575,#36576,#36577,#36578,#36579,#36580,#36581,#36582,#36583,
#36584,#36585,#36586,#36587,#36588,#36589,#36590,#36591,#36592,#36593,#36594,
#36595,#36596,#36597,#36598,#36599,#36600,#36601,#36602,#36603,#36604,#36605,
#36606,#36607,#36608,#36609,#36610,#36611,#36612,#36613,#36614,#36615,#36616,
#36617,#36618,#36619,#36620,#36621,#36622,#36623,#36624,#36625,#36626,#36627,
#36628,#36629,#36630,#36631,#36632,#36633,#36634,#36635,#36636,#36637,#36638,
#36639,#36640,#36641,#36642,#36643,#36644,#36645,#36646,#36647,#36648,#36649,
#36650),(#36651,#36652,#36653,#36654,#36655,#36656,#36657,#36658,#36659,
#36660,#36661,#36662,#36663,#36664,#36665,#36666,#36667,#36668,#36669,#36670,
#36671,#36672,#36673,#36674,#36675,#36676,#36677,#36678,#36679,#36680,#36681,
#36682,#36683,#36684,#36685,#36686,#36687,#36688,#36689,#36690,#36691,#36692,
#36693,#36694,#36695,#36696,#36697,#36698,#36699,#36700,#36701,#36702,#36703,
#36704,#36705,#36706,#36707,#36708,#36709,#36710,#36711,#36712,#36713,#36714,
#36715,#36716,#36717,#36718,#36719,#36720,#36721,#36722,#36723,#36724,#36725,
#36726,#36727,#36728,#36729,#36730,#36731,#36732,#36733,#36734,#36735,#36736,
#36737,#36738,#36739,#36740,#36741,#36742,#36743,#36744,#36745,#36746,#36747,
#36748,#36749,#36750,#36751,#36752,#36753,#36754,#36755,#36756,#36757,#36758,
#36759,#36760,#36761,#36762,#36763,#36764,#36765)),.UNSPECIFIED.,.F.,.F.,
 .F.,(4,4),(4,1,1,1,1,1,1,1,1,1,1,1,1,1,1,1,1,1,1,1,1,1,1,1,1,1,1,1,1,1,
1,1,1,1,1,1,1,1,1,1,1,1,1,1,1,1,1,1,1,1,1,1,1,1,1,1,1,1,1,1,1,1,1,1,1,1,
1,1,1,1,1,1,1,1,1,1,1,1,1,1,1,1,1,1,1,1,1,1,1,1,1,1,1,1,1,1,1,1,1,1,1,1,
1,1,1,1,1,1,1,1,1,1,4),(0.,0.173020531651036),(12.1475814751569,12.6421543672732,
13.1367272593894,13.6313001515056,14.1258730436219,14.6204459357381,15.1150188278544,
15.6095917199706,16.1041646120869,16.5987375042031,17.0933103963194,17.5878832884356,
18.0824561805519,18.5770290726681,19.0716019647843,19.5661748569006,20.0607477490168,
20.5553206411331,21.0498935332493,21.5444664253656,22.0390393174818,22.5336122095981,
23.0281851017143,23.5227579938306,24.0173308859468,24.511903778063,25.0064766701793,
25.5010495622955,25.9956224544118,26.490195346528,26.9847682386443,27.4793411307605,
27.9739140228768,28.468486914993,28.9630598071093,29.4576326992255,29.9522055913417,
30.446778483458,30.9413513755742,31.4359242676905,31.9304971598067,32.425070051923,
32.9196429440392,33.4142158361555,33.9087887282717,34.403361620388,34.8979345125042,
35.3925074046204,35.8870802967367,36.3816531888529,36.8762260809692,37.3707989730854,
37.8653718652017,38.3599447573179,38.8545176494342,39.3490905415504,39.8436634336667,
40.3382363257829,40.8328092178991,41.3273821100154,41.8219550021316,42.3165278942479,
42.8111007863641,43.3056736784804,43.8002465705966,44.2948194627129,44.7893923548291,
45.2839652469454,45.7785381390616,46.2731110311778,46.7676839232941,47.2622568154103,
47.7568297075266,48.2514025996428,48.7459754917591,49.2405483838753,49.7351212759916,
50.2296941681078,50.7242670602241,51.2188399523403,51.7134128444565,52.2079857365728,
52.702558628689,53.1971315208053,53.6917044129215,54.1862773050378,54.680850197154,
55.1754230892703,55.6699959813865,56.1645688735028,56.659141765619,57.1537146577353,
57.6482875498515,58.1428604419677,58.637433334084,59.1320062262002,59.6265791183165,
60.1211520104327,60.615724902549,61.1102977946652,61.6048706867815,62.0994435788977,
62.5940164710139,63.0885893631302,63.5831622552464,64.0777351473627,64.5723080394789,
65.0668809315952,65.5614538237114,66.0560267158277,66.5505996079439,67.0451725000601,
67.5397453921764),.UNSPECIFIED.);
#12=B_SPLINE_SURFACE_WITH_KNOTS('',3,3,((#36865,#36866,#36867,#36868,#36869,
#36870,#36871,#36872,#36873,#36874,#36875,#36876,#36877,#36878,#36879,#36880,
#36881,#36882,#36883,#36884,#36885,#36886,#36887,#36888,#36889,#36890,#36891,
#36892,#36893,#36894,#36895,#36896,#36897,#36898,#36899,#36900,#36901,#36902,
#36903,#36904,#36905,#36906,#36907,#36908,#36909,#36910,#36911,#36912,#36913,
#36914,#36915,#36916,#36917,#36918,#36919,#36920,#36921,#36922,#36923,#36924,
#36925,#36926,#36927,#36928,#36929,#36930,#36931,#36932,#36933,#36934,#36935,
#36936,#36937,#36938,#36939,#36940,#36941,#36942,#36943,#36944,#36945,#36946,
#36947,#36948,#36949,#36950,#36951,#36952,#36953,#36954,#36955,#36956,#36957,
#36958,#36959,#36960,#36961,#36962,#36963,#36964,#36965,#36966,#36967,#36968,
#36969,#36970,#36971,#36972,#36973,#36974,#36975,#36976,#36977,#36978,#36979),
(#36980,#36981,#36982,#36983,#36984,#36985,#36986,#36987,#36988,#36989,
#36990,#36991,#36992,#36993,#36994,#36995,#36996,#36997,#36998,#36999,#37000,
#37001,#37002,#37003,#37004,#37005,#37006,#37007,#37008,#37009,#37010,#37011,
#37012,#37013,#37014,#37015,#37016,#37017,#37018,#37019,#37020,#37021,#37022,
#37023,#37024,#37025,#37026,#37027,#37028,#37029,#37030,#37031,#37032,#37033,
#37034,#37035,#37036,#37037,#37038,#37039,#37040,#37041,#37042,#37043,#37044,
#37045,#37046,#37047,#37048,#37049,#37050,#37051,#37052,#37053,#37054,#37055,
#37056,#37057,#37058,#37059,#37060,#37061,#37062,#37063,#37064,#37065,#37066,
#37067,#37068,#37069,#37070,#37071,#37072,#37073,#37074,#37075,#37076,#37077,
#37078,#37079,#37080,#37081,#37082,#37083,#37084,#37085,#37086,#37087,#37088,
#37089,#37090,#37091,#37092,#37093,#37094),(#37095,#37096,#37097,#37098,
#37099,#37100,#37101,#37102,#37103,#37104,#37105,#37106,#37107,#37108,#37109,
#37110,#37111,#37112,#37113,#37114,#37115,#37116,#37117,#37118,#37119,#37120,
#37121,#37122,#37123,#37124,#37125,#37126,#37127,#37128,#37129,#37130,#37131,
#37132,#37133,#37134,#37135,#37136,#37137,#37138,#37139,#37140,#37141,#37142,
#37143,#37144,#37145,#37146,#37147,#37148,#37149,#37150,#37151,#37152,#37153,
#37154,#37155,#37156,#37157,#37158,#37159,#37160,#37161,#37162,#37163,#37164,
#37165,#37166,#37167,#37168,#37169,#37170,#37171,#37172,#37173,#37174,#37175,
#37176,#37177,#37178,#37179,#37180,#37181,#37182,#37183,#37184,#37185,#37186,
#37187,#37188,#37189,#37190,#37191,#37192,#37193,#37194,#37195,#37196,#37197,
#37198,#37199,#37200,#37201,#37202,#37203,#37204,#37205,#37206,#37207,#37208,
#37209),(#37210,#37211,#37212,#37213,#37214,#37215,#37216,#37217,#37218,
#37219,#37220,#37221,#37222,#37223,#37224,#37225,#37226,#37227,#37228,#37229,
#37230,#37231,#37232,#37233,#37234,#37235,#37236,#37237,#37238,#37239,#37240,
#37241,#37242,#37243,#37244,#37245,#37246,#37247,#37248,#37249,#37250,#37251,
#37252,#37253,#37254,#37255,#37256,#37257,#37258,#37259,#37260,#37261,#37262,
#37263,#37264,#37265,#37266,#37267,#37268,#37269,#37270,#37271,#37272,#37273,
#37274,#37275,#37276,#37277,#37278,#37279,#37280,#37281,#37282,#37283,#37284,
#37285,#37286,#37287,#37288,#37289,#37290,#37291,#37292,#37293,#37294,#37295,
#37296,#37297,#37298,#37299,#37300,#37301,#37302,#37303,#37304,#37305,#37306,
#37307,#37308,#37309,#37310,#37311,#37312,#37313,#37314,#37315,#37316,#37317,
#37318,#37319,#37320,#37321,#37322,#37323,#37324)),.UNSPECIFIED.,.F.,.F.,
 .F.,(4,4),(4,1,1,1,1,1,1,1,1,1,1,1,1,1,1,1,1,1,1,1,1,1,1,1,1,1,1,1,1,1,
1,1,1,1,1,1,1,1,1,1,1,1,1,1,1,1,1,1,1,1,1,1,1,1,1,1,1,1,1,1,1,1,1,1,1,1,
1,1,1,1,1,1,1,1,1,1,1,1,1,1,1,1,1,1,1,1,1,1,1,1,1,1,1,1,1,1,1,1,1,1,1,1,
1,1,1,1,1,1,1,1,1,1,4),(0.,0.173020531651036),(15.1888611523549,15.6834340444711,
16.1780069365874,16.6725798287036,17.1671527208199,17.6617256129361,18.1562985050523,
18.6508713971686,19.1454442892848,19.6400171814011,20.1345900735173,20.6291629656336,
21.1237358577498,21.6183087498661,22.1128816419823,22.6074545340986,23.1020274262148,
23.596600318331,24.0911732104473,24.5857461025635,25.0803189946798,25.574891886796,
26.0694647789123,26.5640376710285,27.0586105631448,27.553183455261,28.0477563473773,
28.5423292394935,29.0369021316097,29.531475023726,30.0260479158422,30.5206208079585,
31.0151937000747,31.509766592191,32.0043394843072,32.4989123764235,32.9934852685397,
33.488058160656,33.9826310527722,34.4772039448884,34.9717768370047,35.4663497291209,
35.9609226212372,36.4554955133534,36.9500684054697,37.4446412975859,37.9392141897022,
38.4337870818184,38.9283599739347,39.4229328660509,39.9175057581671,40.4120786502834,
40.9066515423996,41.4012244345159,41.8957973266321,42.3903702187484,42.8849431108646,
43.3795160029809,43.8740888950971,44.3686617872134,44.8632346793296,45.3578075714458,
45.8523804635621,46.3469533556783,46.8415262477946,47.3360991399108,47.8306720320271,
48.3252449241433,48.8198178162596,49.3143907083758,49.8089636004921,50.3035364926083,
50.7981093847245,51.2926822768408,51.787255168957,52.2818280610733,52.7764009531895,
53.2709738453058,53.765546737422,54.2601196295383,54.7546925216545,55.2492654137708,
55.743838305887,56.2384111980032,56.7329840901195,57.2275569822357,57.722129874352,
58.2167027664682,58.7112756585845,59.2058485507007,59.700421442817,60.1949943349332,
60.6895672270495,61.1841401191657,61.6787130112819,62.1732859033982,62.6678587955144,
63.1624316876307,63.6570045797469,64.1515774718632,64.6461503639794,65.1407232560957,
65.6352961482119,66.1298690403281,66.6244419324444,67.1190148245607,67.6135877166769,
68.1081606087931,68.6027335009094,69.0973063930256,69.5918792851419,70.0864521772581,
70.5810250693744),.UNSPECIFIED.);
#725=B_SPLINE_CURVE_WITH_KNOTS('',3,(#35262,#35263,#35264,#35265,#35266,
#35267,#35268,#35269,#35270,#35271,#35272,#35273,#35274,#35275,#35276,#35277,
#35278,#35279,#35280,#35281,#35282,#35283,#35284,#35285,#35286),
 .UNSPECIFIED.,.F.,.F.,(4,3,3,3,3,3,3,3,4),(-3.56038179279204,-3.46201024481372,
-2.96743735269747,-2.47286446058123,-1.97829156846498,-1.48371867634874,
-0.989145784232491,-0.494572892116246,0.),.UNSPECIFIED.);
#726=B_SPLINE_CURVE_WITH_KNOTS('',3,(#35289,#35290,#35291,#35292,#35293,
#35294,#35295,#35296,#35297,#35298,#35299,#35300,#35301,#35302,#35303,#35304,
#35305,#35306,#35307,#35308,#35309,#35310,#35311,#35312,#35313,#35314,#35315,
#35316,#35317,#35318,#35319,#35320,#35321,#35322,#35323,#35324,#35325,#35326,
#35327,#35328),.UNSPECIFIED.,.F.,.F.,(4,3,3,3,3,3,3,3,3,3,3,3,3,4),(0.937891254796418,
0.989145784232494,1.48371867634874,1.97829156846498,2.47286446058123,2.96743735269748,
3.46201024481372,3.95658313692997,4.45115602904621,4.94572892116246,5.44030181327871,
5.93487470539495,6.42944759751119,6.80228742277363),.UNSPECIFIED.);
#727=B_SPLINE_CURVE_WITH_KNOTS('',3,(#35333,#35334,#35335,#35336,#35337,
#35338,#35339,#35340,#35341,#35342,#35343,#35344,#35345,#35346,#35347,#35348,
#35349,#35350,#35351,#35352,#35353,#35354,#35355,#35356,#35357,#35358,#35359,
#35360,#35361,#35362,#35363,#35364,#35365,#35366,#35367,#35368,#35369,#35370,
#35371,#35372),.UNSPECIFIED.,.F.,.F.,(4,3,3,3,3,3,3,3,3,3,3,3,3,4),(-9.8435670999716,
-9.39688495020867,-8.90231205809242,-8.40773916597618,-7.91316627385993,
-7.41859338174369,-6.92402048962744,-6.42944759751119,-5.93487470539495,
-5.4403018132787,-4.94572892116246,-4.45115602904621,-3.95658313692996,
-3.56038179279204),.UNSPECIFIED.);
#728=B_SPLINE_CURVE_WITH_KNOTS('',3,(#35373,#35374,#35375,#35376,#35377,
#35378,#35379,#35380,#35381,#35382,#35383,#35384,#35385,#35386,#35387,#35388,
#35389,#35390,#35391,#35392,#35393,#35394,#35395,#35396,#35397,#35398,#35399,
#35400,#35401,#35402,#35403,#35404,#35405,#35406,#35407,#35408,#35409,#35410,
#35411,#35412,#35413,#35414,#35415),.UNSPECIFIED.,.F.,.F.,(4,3,3,3,3,3,
3,3,3,3,3,3,3,3,4),(6.80228742277363,6.92402048962744,7.41859338174369,
7.91316627385993,8.40773916597617,8.90231205809242,9.39688495020867,9.89145784232491,
10.3860307344412,10.8806036265574,11.3751765186736,11.8697494107899,12.3643223029061,
12.8588951950224,13.0854727299532),.UNSPECIFIED.);
#729=B_SPLINE_CURVE_WITH_KNOTS('',3,(#35420,#35421,#35422,#35423,#35424,
#35425,#35426,#35427,#35428,#35429,#35430,#35431,#35432,#35433,#35434,#35435,
#35436,#35437,#35438,#35439,#35440,#35441,#35442,#35443,#35444,#35445,#35446,
#35447,#35448,#35449,#35450,#35451,#35452,#35453,#35454,#35455,#35456,#35457,
#35458,#35459,#35460,#35461,#35462),.UNSPECIFIED.,.F.,.F.,(4,3,3,3,3,3,
3,3,3,3,3,3,3,3,4),(-16.1267524071512,-15.8263325477199,-15.3317596556036,
-14.8371867634874,-14.3426138713711,-13.8480409792549,-13.3534680871386,
-12.8588951950224,-12.3643223029061,-11.8697494107899,-11.3751765186736,
-10.8806036265574,-10.3860307344412,-9.89145784232491,-9.8435670999716),
 .UNSPECIFIED.);
#730=B_SPLINE_CURVE_WITH_KNOTS('',3,(#35463,#35464,#35465,#35466,#35467,
#35468,#35469,#35470,#35471,#35472,#35473,#35474,#35475,#35476,#35477,#35478,
#35479,#35480,#35481,#35482,#35483,#35484,#35485,#35486,#35487,#35488,#35489,
#35490,#35491,#35492,#35493,#35494,#35495,#35496,#35497,#35498,#35499,#35500,
#35501,#35502,#35503,#35504,#35505),.UNSPECIFIED.,.F.,.F.,(4,3,3,3,3,3,
3,3,3,3,3,3,3,3,4),(13.0854727299532,13.3534680871386,13.8480409792549,
14.3426138713711,14.8371867634874,15.3317596556036,15.8263325477199,16.3209054398361,
16.8154783319523,17.3100512240686,17.8046241161848,18.2991970083011,18.7937699004173,
19.2883427925336,19.3686580371328),.UNSPECIFIED.);
#731=B_SPLINE_CURVE_WITH_KNOTS('',3,(#35510,#35511,#35512,#35513,#35514,
#35515,#35516,#35517,#35518,#35519,#35520,#35521,#35522,#35523,#35524,#35525,
#35526,#35527,#35528,#35529,#35530,#35531,#35532,#35533,#35534,#35535,#35536,
#35537,#35538,#35539,#35540,#35541,#35542,#35543,#35544,#35545,#35546,#35547,
#35548,#35549,#35550,#35551,#35552),.UNSPECIFIED.,.F.,.F.,(4,3,3,3,3,3,
3,3,3,3,3,3,3,3,4),(-22.4099377143308,-22.2557801452311,-21.7612072531148,
-21.2666343609986,-20.7720614688823,-20.2774885767661,-19.7829156846498,
-19.2883427925336,-18.7937699004173,-18.2991970083011,-17.8046241161848,
-17.3100512240686,-16.8154783319523,-16.3209054398361,-16.1267524071512),
 .UNSPECIFIED.);
#732=B_SPLINE_CURVE_WITH_KNOTS('',3,(#35553,#35554,#35555,#35556,#35557,
#35558,#35559,#35560,#35561,#35562,#35563,#35564,#35565,#35566,#35567,#35568,
#35569,#35570,#35571,#35572,#35573,#35574,#35575,#35576,#35577,#35578,#35579,
#35580,#35581,#35582,#35583,#35584,#35585,#35586,#35587,#35588,#35589,#35590,
#35591,#35592),.UNSPECIFIED.,.F.,.F.,(4,3,3,3,3,3,3,3,3,3,3,3,3,4),(19.3686580371328,
19.7829156846498,20.2774885767661,20.7720614688823,21.2666343609986,21.7612072531148,
22.255780145231,22.7503530373473,23.2449259294635,23.7394988215798,24.234071713696,
24.7286446058123,25.2232174979285,25.6518433443124),.UNSPECIFIED.);
#733=B_SPLINE_CURVE_WITH_KNOTS('',3,(#35597,#35598,#35599,#35600,#35601,
#35602,#35603,#35604,#35605,#35606,#35607,#35608,#35609,#35610,#35611,#35612,
#35613,#35614,#35615,#35616,#35617,#35618,#35619,#35620,#35621,#35622,#35623,
#35624,#35625,#35626,#35627,#35628,#35629,#35630,#35631,#35632,#35633,#35634,
#35635,#35636,#35637,#35638,#35639),.UNSPECIFIED.,.F.,.F.,(4,3,3,3,3,3,
3,3,3,3,3,3,3,3,4),(-28.6931230215104,-28.6852277427422,-28.190654850626,
-27.6960819585097,-27.2015090663935,-26.7069361742773,-26.212363282161,
-25.7177903900448,-25.2232174979285,-24.7286446058123,-24.234071713696,
-23.7394988215798,-23.2449259294635,-22.7503530373473,-22.4099377143308),
 .UNSPECIFIED.);
#734=B_SPLINE_CURVE_WITH_KNOTS('',3,(#35640,#35641,#35642,#35643,#35644,
#35645,#35646,#35647,#35648,#35649,#35650,#35651,#35652,#35653,#35654,#35655,
#35656,#35657,#35658,#35659,#35660,#35661,#35662,#35663,#35664,#35665,#35666,
#35667,#35668,#35669,#35670,#35671,#35672,#35673,#35674,#35675,#35676,#35677,
#35678,#35679,#35680,#35681,#35682),.UNSPECIFIED.,.F.,.F.,(4,3,3,3,3,3,
3,3,3,3,3,3,3,3,4),(25.6518433443124,25.7177903900448,26.212363282161,26.7069361742773,
27.2015090663935,27.6960819585097,28.190654850626,28.6852277427422,29.1798006348585,
29.6743735269747,30.168946419091,30.6635193112072,31.1580922033235,31.6526650954397,
31.935028651492),.UNSPECIFIED.);
#735=B_SPLINE_CURVE_WITH_KNOTS('',3,(#35687,#35688,#35689,#35690,#35691,
#35692,#35693,#35694,#35695,#35696,#35697,#35698,#35699,#35700,#35701,#35702,
#35703,#35704,#35705,#35706,#35707,#35708,#35709,#35710,#35711,#35712,#35713,
#35714,#35715,#35716,#35717,#35718,#35719,#35720,#35721,#35722,#35723,#35724,
#35725,#35726),.UNSPECIFIED.,.F.,.F.,(4,3,3,3,3,3,3,3,3,3,3,3,3,4),(-34.97630832869,
-34.6201024481372,-34.1255295560209,-33.6309566639047,-33.1363837717884,
-32.6418108796722,-32.147237987556,-31.6526650954397,-31.1580922033235,
-30.6635193112072,-30.168946419091,-29.6743735269747,-29.1798006348585,
-28.6931230215104),.UNSPECIFIED.);
#736=B_SPLINE_CURVE_WITH_KNOTS('',3,(#35727,#35728,#35729,#35730,#35731,
#35732,#35733,#35734,#35735,#35736,#35737,#35738,#35739,#35740,#35741,#35742,
#35743,#35744,#35745,#35746,#35747,#35748,#35749,#35750,#35751,#35752,#35753,
#35754,#35755,#35756,#35757,#35758,#35759,#35760,#35761,#35762,#35763,#35764,
#35765,#35766,#35767,#35768,#35769),.UNSPECIFIED.,.F.,.F.,(4,3,3,3,3,3,
3,3,3,3,3,3,3,3,4),(31.935028651492,32.147237987556,32.6418108796722,33.1363837717885,
33.6309566639047,34.1255295560209,34.6201024481372,35.1146753402534,35.6092482323697,
36.1038211244859,36.5983940166022,37.0929669087184,37.5875398008347,38.0821126929509,
38.2182139586716),.UNSPECIFIED.);
#737=B_SPLINE_CURVE_WITH_KNOTS('',3,(#35774,#35775,#35776,#35777,#35778,
#35779,#35780,#35781,#35782,#35783,#35784,#35785,#35786,#35787,#35788,#35789,
#35790,#35791,#35792,#35793,#35794,#35795,#35796,#35797,#35798,#35799,#35800,
#35801,#35802,#35803,#35804,#35805,#35806,#35807,#35808,#35809,#35810,#35811,
#35812,#35813,#35814,#35815,#35816),.UNSPECIFIED.,.F.,.F.,(4,3,3,3,3,3,
3,3,3,3,3,3,3,3,4),(-41.2594936358696,-41.0495500456484,-40.5549771535321,
-40.0604042614159,-39.5658313692996,-39.0712584771834,-38.5766855850671,
-38.0821126929509,-37.5875398008347,-37.0929669087184,-36.5983940166022,
-36.1038211244859,-35.6092482323697,-35.1146753402534,-34.97630832869),
 .UNSPECIFIED.);
#738=B_SPLINE_CURVE_WITH_KNOTS('',3,(#35817,#35818,#35819,#35820,#35821,
#35822,#35823,#35824,#35825,#35826,#35827,#35828,#35829,#35830,#35831,#35832,
#35833,#35834,#35835,#35836,#35837,#35838,#35839,#35840,#35841,#35842,#35843,
#35844,#35845,#35846,#35847,#35848,#35849,#35850,#35851,#35852,#35853,#35854,
#35855,#35856),.UNSPECIFIED.,.F.,.F.,(4,3,3,3,3,3,3,3,3,3,3,3,3,4),(38.2182139586716,
38.5766855850671,39.0712584771834,39.5658313692996,40.0604042614159,40.5549771535321,
41.0495500456484,41.5441229377646,42.0386958298809,42.5332687219971,43.0278416141134,
43.5224145062296,44.0169873983459,44.5013992658512),.UNSPECIFIED.);
#739=B_SPLINE_CURVE_WITH_KNOTS('',3,(#35861,#35862,#35863,#35864,#35865,
#35866,#35867,#35868,#35869,#35870,#35871,#35872,#35873,#35874,#35875,#35876,
#35877,#35878,#35879,#35880,#35881,#35882,#35883,#35884,#35885,#35886,#35887,
#35888,#35889,#35890,#35891,#35892,#35893,#35894,#35895,#35896,#35897,#35898,
#35899,#35900,#35901,#35902,#35903),.UNSPECIFIED.,.F.,.F.,(4,3,3,3,3,3,
3,3,3,3,3,3,3,3,4),(-47.5426789430491,-47.4789976431596,-46.9844247510433,
-46.4898518589271,-45.9952789668108,-45.5007060746946,-45.0061331825783,
-44.5115602904621,-44.0169873983458,-43.5224145062296,-43.0278416141134,
-42.5332687219971,-42.0386958298809,-41.5441229377646,-41.2594936358696),
 .UNSPECIFIED.);
#740=B_SPLINE_CURVE_WITH_KNOTS('',3,(#35904,#35905,#35906,#35907,#35908,
#35909,#35910,#35911,#35912,#35913,#35914,#35915,#35916,#35917,#35918,#35919,
#35920,#35921,#35922,#35923,#35924,#35925,#35926,#35927,#35928,#35929,#35930,
#35931,#35932,#35933,#35934,#35935,#35936,#35937,#35938,#35939,#35940,#35941,
#35942,#35943,#35944,#35945,#35946),.UNSPECIFIED.,.F.,.F.,(4,3,3,3,3,3,
3,3,3,3,3,3,3,3,4),(44.5013992658512,44.5115602904621,45.0061331825783,
45.5007060746946,45.9952789668108,46.4898518589271,46.9844247510433,47.4789976431596,
47.9735705352758,48.4681434273921,48.9627163195083,49.4572892116245,49.9518621037408,
50.446434995857,50.7845845730308),.UNSPECIFIED.);
#741=B_SPLINE_CURVE_WITH_KNOTS('',3,(#35953,#35954,#35955,#35956,#35957,
#35958,#35959,#35960,#35961,#35962),.UNSPECIFIED.,.F.,.F.,(4,3,3,4),(-54.4542726622231,
-54.403018132787,-53.9084452406708,-53.8258642502287),.UNSPECIFIED.);
#742=B_SPLINE_CURVE_WITH_KNOTS('',3,(#35968,#35969,#35970,#35971,#35972,
#35973,#35974),.UNSPECIFIED.,.F.,.F.,(4,1,1,1,4),(65.9734457253856,66.0560267158277,
66.5505996079439,67.0451725000601,67.5397453921764),.UNSPECIFIED.);
#743=B_SPLINE_CURVE_WITH_KNOTS('',3,(#35977,#35978,#35979,#35980,#35981,
#35982,#35983,#35984,#35985,#35986,#35987,#35988),.UNSPECIFIED.,.F.,.F.,
(4,1,1,1,1,1,1,1,1,4),(65.9734457253856,66.1298690403281,66.6244419324444,
67.1190148245607,67.6135877166769,68.1081606087931,68.6027335009094,69.0973063930256,
69.5918792851419,69.643133814578),.UNSPECIFIED.);
#744=B_SPLINE_CURVE_WITH_KNOTS('',3,(#35993,#35994,#35995,#35996,#35997,
#35998,#35999,#36000,#36001,#36002,#36003,#36004,#36005,#36006,#36007,#36008),
 .UNSPECIFIED.,.F.,.F.,(4,1,1,1,1,1,1,1,1,1,1,1,1,4),(59.6902604182061,
60.1211520104327,60.615724902549,61.1102977946652,61.6048706867815,62.0994435788977,
62.5940164710139,63.0885893631302,63.5831622552464,64.0777351473627,64.5723080394789,
65.0668809315952,65.5614538237114,65.9734457253856),.UNSPECIFIED.);
#745=B_SPLINE_CURVE_WITH_KNOTS('',3,(#36009,#36010,#36011,#36012,#36013,
#36014,#36015,#36016,#36017,#36018,#36019,#36020,#36021,#36022,#36023,#36024,
#36025),.UNSPECIFIED.,.F.,.F.,(4,1,1,1,1,1,1,1,1,1,1,1,1,1,4),(59.6902604182061,
59.700421442817,60.1949943349332,60.6895672270495,61.1841401191657,61.6787130112819,
62.1732859033982,62.6678587955144,63.1624316876307,63.6570045797469,64.1515774718632,
64.6461503639794,65.1407232560957,65.6352961482119,65.9734457253856),
 .UNSPECIFIED.);
#746=B_SPLINE_CURVE_WITH_KNOTS('',3,(#36030,#36031,#36032,#36033,#36034,
#36035,#36036,#36037,#36038,#36039,#36040,#36041,#36042,#36043,#36044,#36045,
#36046),.UNSPECIFIED.,.F.,.F.,(4,1,1,1,1,1,1,1,1,1,1,1,1,1,4),(53.4070751110264,
53.6917044129215,54.1862773050378,54.680850197154,55.1754230892703,55.6699959813865,
56.1645688735028,56.659141765619,57.1537146577353,57.6482875498515,58.1428604419677,
58.637433334084,59.1320062262002,59.6265791183165,59.6902604182061),
 .UNSPECIFIED.);
#747=B_SPLINE_CURVE_WITH_KNOTS('',3,(#36047,#36048,#36049,#36050,#36051,
#36052,#36053,#36054,#36055,#36056,#36057,#36058,#36059,#36060,#36061,#36062),
 .UNSPECIFIED.,.F.,.F.,(4,1,1,1,1,1,1,1,1,1,1,1,1,4),(53.4070751110264,
53.765546737422,54.2601196295383,54.7546925216545,55.2492654137708,55.743838305887,
56.2384111980032,56.7329840901195,57.2275569822357,57.722129874352,58.2167027664682,
58.7112756585845,59.2058485507007,59.6902604182061),.UNSPECIFIED.);
#748=B_SPLINE_CURVE_WITH_KNOTS('',3,(#36067,#36068,#36069,#36070,#36071,
#36072,#36073,#36074,#36075,#36076,#36077,#36078,#36079,#36080,#36081,#36082,
#36083),.UNSPECIFIED.,.F.,.F.,(4,1,1,1,1,1,1,1,1,1,1,1,1,1,4),(47.1238898038469,
47.2622568154103,47.7568297075266,48.2514025996428,48.7459754917591,49.2405483838753,
49.7351212759916,50.2296941681078,50.7242670602241,51.2188399523403,51.7134128444565,
52.2079857365728,52.702558628689,53.1971315208053,53.4070751110264),
 .UNSPECIFIED.);
#749=B_SPLINE_CURVE_WITH_KNOTS('',3,(#36084,#36085,#36086,#36087,#36088,
#36089,#36090,#36091,#36092,#36093,#36094,#36095,#36096,#36097,#36098,#36099,
#36100),.UNSPECIFIED.,.F.,.F.,(4,1,1,1,1,1,1,1,1,1,1,1,1,1,4),(47.1238898038469,
47.3360991399108,47.8306720320271,48.3252449241433,48.8198178162596,49.3143907083758,
49.8089636004921,50.3035364926083,50.7981093847245,51.2926822768408,51.787255168957,
52.2818280610733,52.7764009531895,53.2709738453058,53.4070751110264),
 .UNSPECIFIED.);
#750=B_SPLINE_CURVE_WITH_KNOTS('',3,(#36105,#36106,#36107,#36108,#36109,
#36110,#36111,#36112,#36113,#36114,#36115,#36116,#36117,#36118,#36119,#36120),
 .UNSPECIFIED.,.F.,.F.,(4,1,1,1,1,1,1,1,1,1,1,1,1,4),(40.8407044966673,
41.3273821100154,41.8219550021316,42.3165278942479,42.8111007863641,43.3056736784804,
43.8002465705966,44.2948194627129,44.7893923548291,45.2839652469454,45.7785381390616,
46.2731110311778,46.7676839232941,47.1238898038469),.UNSPECIFIED.);
#751=B_SPLINE_CURVE_WITH_KNOTS('',3,(#36121,#36122,#36123,#36124,#36125,
#36126,#36127,#36128,#36129,#36130,#36131,#36132,#36133,#36134,#36135,#36136,
#36137),.UNSPECIFIED.,.F.,.F.,(4,1,1,1,1,1,1,1,1,1,1,1,1,1,4),(40.8407044966673,
40.9066515423996,41.4012244345159,41.8957973266321,42.3903702187484,42.8849431108646,
43.3795160029809,43.8740888950971,44.3686617872134,44.8632346793296,45.3578075714458,
45.8523804635621,46.3469533556783,46.8415262477946,47.1238898038469),
 .UNSPECIFIED.);
#752=B_SPLINE_CURVE_WITH_KNOTS('',3,(#36142,#36143,#36144,#36145,#36146,
#36147,#36148,#36149,#36150,#36151,#36152,#36153,#36154,#36155,#36156,#36157,
#36158),.UNSPECIFIED.,.F.,.F.,(4,1,1,1,1,1,1,1,1,1,1,1,1,1,4),(34.5575191894877,
34.8979345125042,35.3925074046204,35.8870802967367,36.3816531888529,36.8762260809692,
37.3707989730854,37.8653718652017,38.3599447573179,38.8545176494342,39.3490905415504,
39.8436634336667,40.3382363257829,40.8328092178991,40.8407044966673),
 .UNSPECIFIED.);
#753=B_SPLINE_CURVE_WITH_KNOTS('',3,(#36159,#36160,#36161,#36162,#36163,
#36164,#36165,#36166,#36167,#36168,#36169,#36170,#36171,#36172,#36173,#36174),
 .UNSPECIFIED.,.F.,.F.,(4,1,1,1,1,1,1,1,1,1,1,1,1,4),(34.5575191894877,
34.9717768370047,35.4663497291209,35.9609226212372,36.4554955133534,36.9500684054697,
37.4446412975859,37.9392141897022,38.4337870818184,38.9283599739347,39.4229328660509,
39.9175057581671,40.4120786502834,40.8407044966673),.UNSPECIFIED.);
#754=B_SPLINE_CURVE_WITH_KNOTS('',3,(#36179,#36180,#36181,#36182,#36183,
#36184,#36185,#36186,#36187,#36188,#36189,#36190,#36191,#36192,#36193,#36194,
#36195),.UNSPECIFIED.,.F.,.F.,(4,1,1,1,1,1,1,1,1,1,1,1,1,1,4),(28.2743338823081,
28.468486914993,28.9630598071093,29.4576326992255,29.9522055913417,30.446778483458,
30.9413513755742,31.4359242676905,31.9304971598067,32.425070051923,32.9196429440392,
33.4142158361555,33.9087887282717,34.403361620388,34.5575191894877),
 .UNSPECIFIED.);
#755=B_SPLINE_CURVE_WITH_KNOTS('',3,(#36196,#36197,#36198,#36199,#36200,
#36201,#36202,#36203,#36204,#36205,#36206,#36207,#36208,#36209,#36210,#36211,
#36212),.UNSPECIFIED.,.F.,.F.,(4,1,1,1,1,1,1,1,1,1,1,1,1,1,4),(28.2743338823081,
28.5423292394935,29.0369021316097,29.531475023726,30.0260479158422,30.5206208079585,
31.0151937000747,31.509766592191,32.0043394843072,32.4989123764235,32.9934852685397,
33.488058160656,33.9826310527722,34.4772039448884,34.5575191894877),
 .UNSPECIFIED.);
#756=B_SPLINE_CURVE_WITH_KNOTS('',3,(#36217,#36218,#36219,#36220,#36221,
#36222,#36223,#36224,#36225,#36226,#36227,#36228,#36229,#36230,#36231,#36232,
#36233),.UNSPECIFIED.,.F.,.F.,(4,1,1,1,1,1,1,1,1,1,1,1,1,1,4),(21.9911485751285,
22.0390393174818,22.5336122095981,23.0281851017143,23.5227579938306,24.0173308859468,
24.511903778063,25.0064766701793,25.5010495622955,25.9956224544118,26.490195346528,
26.9847682386443,27.4793411307605,27.9739140228768,28.2743338823081),
 .UNSPECIFIED.);
#757=B_SPLINE_CURVE_WITH_KNOTS('',3,(#36234,#36235,#36236,#36237,#36238,
#36239,#36240,#36241,#36242,#36243,#36244,#36245,#36246,#36247,#36248,#36249,
#36250),.UNSPECIFIED.,.F.,.F.,(4,1,1,1,1,1,1,1,1,1,1,1,1,1,4),(21.9911485751285,
22.1128816419823,22.6074545340986,23.1020274262148,23.596600318331,24.0911732104473,
24.5857461025635,25.0803189946798,25.574891886796,26.0694647789123,26.5640376710285,
27.0586105631448,27.553183455261,28.0477563473773,28.2743338823081),
 .UNSPECIFIED.);
#758=B_SPLINE_CURVE_WITH_KNOTS('',3,(#36256,#36257,#36258,#36259,#36260),
 .UNSPECIFIED.,.F.,.F.,(4,1,4),(15.1888611523549,15.6834340444711,15.7079632679489),
 .UNSPECIFIED.);
#759=B_SPLINE_CURVE_WITH_KNOTS('',3,(#36263,#36264,#36265,#36266,#36267,
#36268,#36269,#36270,#36271,#36272),.UNSPECIFIED.,.F.,.F.,(4,1,1,1,1,1,
1,4),(13.0854727299533,13.1367272593894,13.6313001515056,14.1258730436219,
14.6204459357381,15.1150188278544,15.6095917199706,15.7079632679489),
 .UNSPECIFIED.);
#760=B_SPLINE_CURVE_WITH_KNOTS('',3,(#36274,#36275,#36276,#36277,#36278,
#36279,#36280,#36281,#36282,#36283,#36284,#36285,#36286,#36287,#36288,#36289),
 .UNSPECIFIED.,.F.,.F.,(4,1,1,1,1,1,1,1,1,1,1,1,1,4),(15.7079632679489,
16.1041646120869,16.5987375042031,17.0933103963194,17.5878832884356,18.0824561805519,
18.5770290726681,19.0716019647843,19.5661748569006,20.0607477490168,20.5553206411331,
21.0498935332493,21.5444664253656,21.9911485751285),.UNSPECIFIED.);
#761=B_SPLINE_CURVE_WITH_KNOTS('',3,(#36290,#36291,#36292,#36293,#36294,
#36295,#36296,#36297,#36298,#36299,#36300,#36301,#36302,#36303,#36304,#36305),
 .UNSPECIFIED.,.F.,.F.,(4,1,1,1,1,1,1,1,1,1,1,1,1,4),(15.7079632679489,
16.1780069365874,16.6725798287036,17.1671527208199,17.6617256129361,18.1562985050523,
18.6508713971686,19.1454442892848,19.6400171814011,20.1345900735173,20.6291629656336,
21.1237358577498,21.6183087498661,21.9911485751285),.UNSPECIFIED.);
#762=B_SPLINE_CURVE_WITH_KNOTS('',3,(#36766,#36767,#36768,#36769,#36770,
#36771,#36772,#36773,#36774,#36775,#36776,#36777,#36778,#36779,#36780,#36781,
#36782,#36783,#36784,#36785,#36786,#36787,#36788,#36789,#36790,#36791,#36792,
#36793,#36794,#36795,#36796),.UNSPECIFIED.,.F.,.F.,(4,3,3,3,3,3,3,3,3,3,
4),(0.,0.0822466706468383,0.162608105240606,0.216579893838171,0.23924274204394,
0.301838371937517,0.36076250940623,0.388067588559334,0.409537377502954,
0.476290104322315,0.53753492181237),.UNSPECIFIED.);
#763=B_SPLINE_CURVE_WITH_KNOTS('',3,(#36797,#36798,#36799,#36800,#36801,
#36802,#36803,#36804,#36805,#36806,#36807,#36808,#36809,#36810,#36811,#36812,
#36813,#36814,#36815,#36816,#36817,#36818,#36819,#36820,#36821,#36822,#36823,
#36824),.UNSPECIFIED.,.F.,.F.,(4,3,3,3,3,3,3,3,3,4),(0.,0.0665230127441691,
0.13429495842692,0.176258819244205,0.195926107024299,0.263526952009386,
0.33682854572103,0.365338415901403,0.449700157257057,0.534061898612711),
 .UNSPECIFIED.);
#764=B_SPLINE_CURVE_WITH_KNOTS('',3,(#36825,#36826,#36827,#36828,#36829,
#36830,#36831,#36832,#36833,#36834,#36835,#36836,#36837,#36838,#36839,#36840,
#36841,#36842,#36843,#36844,#36845,#36846,#36847,#36848,#36849,#36850,#36851,
#36852,#36853,#36854,#36855,#36856,#36857,#36858,#36859,#36860,#36861,#36862,
#36863,#36864),.UNSPECIFIED.,.F.,.F.,(4,3,3,3,3,3,3,3,3,3,3,3,3,4),(-53.8258642502287,
-53.4138723485545,-52.9192994564383,-52.424726564322,-51.9301536722058,
-51.4355807800895,-50.9410078879733,-50.446434995857,-49.9518621037408,
-49.4572892116245,-48.9627163195083,-48.4681434273921,-47.9735705352758,
-47.5426789430491),.UNSPECIFIED.);
#765=B_SPLINE_CURVE_WITH_KNOTS('',3,(#37326,#37327,#37328,#37329,#37330,
#37331,#37332,#37333,#37334,#37335,#37336,#37337,#37338,#37339,#37340,#37341,
#37342,#37343,#37344,#37345,#37346,#37347,#37348,#37349,#37350,#37351,#37352,
#37353),.UNSPECIFIED.,.F.,.F.,(4,3,3,3,3,3,3,3,3,4),(0.,0.0665230199567328,
0.134294967830964,0.176258831509978,0.195926124443112,0.263526952009376,
0.336828549458816,0.365338416771381,0.449700157692121,0.534061898612861),
 .UNSPECIFIED.);
#766=B_SPLINE_CURVE_WITH_KNOTS('',3,(#37354,#37355,#37356,#37357,#37358,
#37359,#37360,#37361,#37362,#37363,#37364,#37365,#37366,#37367,#37368,#37369,
#37370,#37371,#37372,#37373,#37374,#37375,#37376,#37377,#37378,#37379,#37380,
#37381,#37382,#37383,#37384),.UNSPECIFIED.,.F.,.F.,(4,3,3,3,3,3,3,3,3,3,
4),(50.7845845730308,50.9410078879733,51.4355807800895,51.9301536722058,
52.424726564322,52.9192994564383,53.4138723485545,53.9084452406708,54.403018132787,
54.8975910249033,55.3921639170195),.UNSPECIFIED.);
#767=B_SPLINE_CURVE_WITH_KNOTS('',3,(#37385,#37386,#37387,#37388,#37389,
#37390,#37391,#37392,#37393,#37394,#37395,#37396,#37397,#37398,#37399,#37400,
#37401,#37402,#37403,#37404,#37405,#37406,#37407,#37408,#37409,#37410,#37411,
#37412,#37413,#37414,#37415),.UNSPECIFIED.,.F.,.F.,(4,3,3,3,3,3,3,3,3,3,
4),(0.,0.0822466663612967,0.162608100396307,0.216579890867136,0.239242742625966,
0.301838371937549,0.360762509406336,0.388067584071394,0.409537375230468,
0.476290092032249,0.537534921812695),.UNSPECIFIED.);
#1533=SHAPE_REPRESENTATION_RELATIONSHIP('SRR','None',#63385,#1616);
#1616=ADVANCED_BREP_SHAPE_REPRESENTATION('',(#1826),#62922);
#1714=STYLED_ITEM('',(#63919),#1826);
#1826=MANIFOLD_SOLID_BREP('Body1',#23009);
#2050=FACE_BOUND('',#4728,.T.);
#2051=FACE_BOUND('',#4729,.T.);
#2052=FACE_BOUND('',#4730,.T.);
#2053=FACE_BOUND('',#4731,.T.);
#2054=FACE_BOUND('',#4737,.T.);
#2055=FACE_BOUND('',#4738,.T.);
#2056=FACE_BOUND('',#4739,.T.);
#2057=FACE_BOUND('',#4740,.T.);
#2058=FACE_BOUND('',#4745,.T.);
#2491=PLANE('',#24776);
#2492=PLANE('',#24788);
#2493=PLANE('',#24789);
#2494=PLANE('',#24796);
#3229=FACE_OUTER_BOUND('',#4706,.T.);
#3230=FACE_OUTER_BOUND('',#4707,.T.);
#3231=FACE_OUTER_BOUND('',#4708,.T.);
#3232=FACE_OUTER_BOUND('',#4709,.T.);
#3233=FACE_OUTER_BOUND('',#4710,.T.);
#3234=FACE_OUTER_BOUND('',#4711,.T.);
#3235=FACE_OUTER_BOUND('',#4712,.T.);
#3236=FACE_OUTER_BOUND('',#4713,.T.);
#3237=FACE_OUTER_BOUND('',#4714,.T.);
#3238=FACE_OUTER_BOUND('',#4715,.T.);
#3239=FACE_OUTER_BOUND('',#4716,.T.);
#3240=FACE_OUTER_BOUND('',#4717,.T.);
#3241=FACE_OUTER_BOUND('',#4718,.T.);
#3242=FACE_OUTER_BOUND('',#4719,.T.);
#3243=FACE_OUTER_BOUND('',#4720,.T.);
#3244=FACE_OUTER_BOUND('',#4721,.T.);
#3245=FACE_OUTER_BOUND('',#4722,.T.);
#3246=FACE_OUTER_BOUND('',#4723,.T.);
#3247=FACE_OUTER_BOUND('',#4724,.T.);
#3248=FACE_OUTER_BOUND('',#4725,.T.);
#3249=FACE_OUTER_BOUND('',#4726,.T.);
#3250=FACE_OUTER_BOUND('',#4727,.T.);
#3251=FACE_OUTER_BOUND('',#4732,.T.);
#3252=FACE_OUTER_BOUND('',#4733,.T.);
#3253=FACE_OUTER_BOUND('',#4734,.T.);
#3254=FACE_OUTER_BOUND('',#4735,.T.);
#3255=FACE_OUTER_BOUND('',#4736,.T.);
#3256=FACE_OUTER_BOUND('',#4741,.T.);
#3257=FACE_OUTER_BOUND('',#4742,.T.);
#3258=FACE_OUTER_BOUND('',#4743,.T.);
#3259=FACE_OUTER_BOUND('',#4744,.T.);
#4706=EDGE_LOOP('',(#16502,#16503,#16504,#16505));
#4707=EDGE_LOOP('',(#16506,#16507,#16508,#16509));
#4708=EDGE_LOOP('',(#16510,#16511,#16512,#16513));
#4709=EDGE_LOOP('',(#16514,#16515,#16516,#16517));
#4710=EDGE_LOOP('',(#16518,#16519,#16520,#16521));
#4711=EDGE_LOOP('',(#16522,#16523,#16524,#16525));
#4712=EDGE_LOOP('',(#16526,#16527,#16528,#16529));
#4713=EDGE_LOOP('',(#16530,#16531,#16532,#16533));
#4714=EDGE_LOOP('',(#16534,#16535,#16536));
#4715=EDGE_LOOP('',(#16537,#16538,#16539,#16540));
#4716=EDGE_LOOP('',(#16541,#16542,#16543,#16544));
#4717=EDGE_LOOP('',(#16545,#16546,#16547,#16548));
#4718=EDGE_LOOP('',(#16549,#16550,#16551,#16552));
#4719=EDGE_LOOP('',(#16553,#16554,#16555,#16556));
#4720=EDGE_LOOP('',(#16557,#16558,#16559,#16560));
#4721=EDGE_LOOP('',(#16561,#16562,#16563,#16564));
#4722=EDGE_LOOP('',(#16565,#16566,#16567,#16568));
#4723=EDGE_LOOP('',(#16569,#16570,#16571,#16572));
#4724=EDGE_LOOP('',(#16573,#16574,#16575,#16576));
#4725=EDGE_LOOP('',(#16577,#16578,#16579,#16580,#16581,#16582,#16583,#16584,
#16585,#16586,#16587,#16588,#16589,#16590,#16591,#16592,#16593,#16594,#16595,
#16596,#16597,#16598));
#4726=EDGE_LOOP('',(#16599,#16600,#16601,#16602,#16603,#16604,#16605,#16606,
#16607,#16608,#16609,#16610,#16611,#16612,#16613,#16614,#16615,#16616,#16617,
#16618,#16619));
#4727=EDGE_LOOP('',(#16620,#16621));
#4728=EDGE_LOOP('',(#16622,#16623,#16624,#16625,#16626));
#4729=EDGE_LOOP('',(#16627));
#4730=EDGE_LOOP('',(#16628));
#4731=EDGE_LOOP('',(#16629));
#4732=EDGE_LOOP('',(#16630,#16631,#16632,#16633));
#4733=EDGE_LOOP('',(#16634,#16635,#16636,#16637));
#4734=EDGE_LOOP('',(#16638,#16639,#16640,#16641));
#4735=EDGE_LOOP('',(#16642,#16643,#16644,#16645));
#4736=EDGE_LOOP('',(#16646,#16647));
#4737=EDGE_LOOP('',(#16648));
#4738=EDGE_LOOP('',(#16649));
#4739=EDGE_LOOP('',(#16650));
#4740=EDGE_LOOP('',(#16651));
#4741=EDGE_LOOP('',(#16652,#16653,#16654,#16655));
#4742=EDGE_LOOP('',(#16656,#16657,#16658,#16659,#16660));
#4743=EDGE_LOOP('',(#16661,#16662,#16663,#16664));
#4744=EDGE_LOOP('',(#16665));
#4745=EDGE_LOOP('',(#16666,#16667,#16668,#16669));
#6330=LINE('',#35260,#7817);
#6331=LINE('',#35332,#7818);
#6332=LINE('',#35419,#7819);
#6333=LINE('',#35509,#7820);
#6334=LINE('',#35596,#7821);
#6335=LINE('',#35686,#7822);
#6336=LINE('',#35773,#7823);
#6337=LINE('',#35860,#7824);
#6338=LINE('',#35950,#7825);
#6339=LINE('',#35966,#7826);
#6340=LINE('',#35992,#7827);
#6341=LINE('',#36029,#7828);
#6342=LINE('',#36066,#7829);
#6343=LINE('',#36104,#7830);
#6344=LINE('',#36141,#7831);
#6345=LINE('',#36178,#7832);
#6346=LINE('',#36216,#7833);
#6347=LINE('',#36254,#7834);
#6348=LINE('',#37419,#7835);
#6349=LINE('',#37431,#7836);
#6350=LINE('',#37435,#7837);
#6351=LINE('',#37439,#7838);
#6352=LINE('',#37443,#7839);
#6353=LINE('',#37444,#7840);
#6354=LINE('',#37445,#7841);
#6355=LINE('',#37454,#7842);
#7817=VECTOR('',#28393,0.45);
#7818=VECTOR('',#28398,0.45);
#7819=VECTOR('',#28401,0.45);
#7820=VECTOR('',#28404,0.45);
#7821=VECTOR('',#28407,0.45);
#7822=VECTOR('',#28410,0.45);
#7823=VECTOR('',#28413,0.45);
#7824=VECTOR('',#28416,0.45);
#7825=VECTOR('',#28419,0.45);
#7826=VECTOR('',#28424,0.625);
#7827=VECTOR('',#28429,0.625);
#7828=VECTOR('',#28432,0.625);
#7829=VECTOR('',#28435,0.625);
#7830=VECTOR('',#28438,0.625);
#7831=VECTOR('',#28441,0.625);
#7832=VECTOR('',#28444,0.625);
#7833=VECTOR('',#28447,0.625);
#7834=VECTOR('',#28450,0.625);
#7835=VECTOR('',#28457,1.);
#7836=VECTOR('',#28472,0.225);
#7837=VECTOR('',#28477,0.225);
#7838=VECTOR('',#28482,0.225);
#7839=VECTOR('',#28485,1.);
#7840=VECTOR('',#28486,1.);
#7841=VECTOR('',#28487,1.);
#7842=VECTOR('',#28500,1.1);
#9223=CIRCLE('',#24754,0.457875);
#9224=CIRCLE('',#24763,0.457875);
#9225=CIRCLE('',#24765,0.625);
#9226=CIRCLE('',#24774,0.625);
#9227=CIRCLE('',#24777,1.9);
#9228=CIRCLE('',#24778,0.457875);
#9229=CIRCLE('',#24779,0.225);
#9230=CIRCLE('',#24780,0.225);
#9231=CIRCLE('',#24781,0.225);
#9232=CIRCLE('',#24783,0.225);
#9233=CIRCLE('',#24785,0.225);
#9234=CIRCLE('',#24787,0.225);
#9235=CIRCLE('',#24790,1.9);
#9236=CIRCLE('',#24791,1.1);
#9237=CIRCLE('',#24795,1.1);
#10319=VERTEX_POINT('',#35258);
#10320=VERTEX_POINT('',#35259);
#10321=VERTEX_POINT('',#35261);
#10322=VERTEX_POINT('',#35287);
#10323=VERTEX_POINT('',#35330);
#10324=VERTEX_POINT('',#35331);
#10325=VERTEX_POINT('',#35417);
#10326=VERTEX_POINT('',#35418);
#10327=VERTEX_POINT('',#35507);
#10328=VERTEX_POINT('',#35508);
#10329=VERTEX_POINT('',#35594);
#10330=VERTEX_POINT('',#35595);
#10331=VERTEX_POINT('',#35684);
#10332=VERTEX_POINT('',#35685);
#10333=VERTEX_POINT('',#35771);
#10334=VERTEX_POINT('',#35772);
#10335=VERTEX_POINT('',#35858);
#10336=VERTEX_POINT('',#35859);
#10337=VERTEX_POINT('',#35948);
#10338=VERTEX_POINT('',#35949);
#10339=VERTEX_POINT('',#35951);
#10340=VERTEX_POINT('',#35964);
#10341=VERTEX_POINT('',#35965);
#10342=VERTEX_POINT('',#35967);
#10343=VERTEX_POINT('',#35975);
#10344=VERTEX_POINT('',#35990);
#10345=VERTEX_POINT('',#35991);
#10346=VERTEX_POINT('',#36027);
#10347=VERTEX_POINT('',#36028);
#10348=VERTEX_POINT('',#36064);
#10349=VERTEX_POINT('',#36065);
#10350=VERTEX_POINT('',#36102);
#10351=VERTEX_POINT('',#36103);
#10352=VERTEX_POINT('',#36139);
#10353=VERTEX_POINT('',#36140);
#10354=VERTEX_POINT('',#36176);
#10355=VERTEX_POINT('',#36177);
#10356=VERTEX_POINT('',#36214);
#10357=VERTEX_POINT('',#36215);
#10358=VERTEX_POINT('',#36252);
#10359=VERTEX_POINT('',#36253);
#10360=VERTEX_POINT('',#36255);
#10361=VERTEX_POINT('',#36261);
#10362=VERTEX_POINT('',#37325);
#10363=VERTEX_POINT('',#37417);
#10364=VERTEX_POINT('',#37418);
#10365=VERTEX_POINT('',#37422);
#10366=VERTEX_POINT('',#37424);
#10367=VERTEX_POINT('',#37426);
#10368=VERTEX_POINT('',#37429);
#10369=VERTEX_POINT('',#37433);
#10370=VERTEX_POINT('',#37437);
#10371=VERTEX_POINT('',#37441);
#10372=VERTEX_POINT('',#37442);
#10373=VERTEX_POINT('',#37448);
#10374=VERTEX_POINT('',#37453);
#12635=EDGE_CURVE('',#10319,#10320,#6330,.T.);
#12636=EDGE_CURVE('',#10320,#10321,#725,.T.);
#12637=EDGE_CURVE('',#10321,#10322,#9223,.F.);
#12638=EDGE_CURVE('',#10322,#10319,#726,.T.);
#12639=EDGE_CURVE('',#10323,#10324,#6331,.T.);
#12640=EDGE_CURVE('',#10324,#10320,#727,.T.);
#12641=EDGE_CURVE('',#10319,#10323,#728,.T.);
#12642=EDGE_CURVE('',#10325,#10326,#6332,.T.);
#12643=EDGE_CURVE('',#10326,#10324,#729,.T.);
#12644=EDGE_CURVE('',#10323,#10325,#730,.T.);
#12645=EDGE_CURVE('',#10327,#10328,#6333,.T.);
#12646=EDGE_CURVE('',#10328,#10326,#731,.T.);
#12647=EDGE_CURVE('',#10325,#10327,#732,.T.);
#12648=EDGE_CURVE('',#10329,#10330,#6334,.T.);
#12649=EDGE_CURVE('',#10330,#10328,#733,.T.);
#12650=EDGE_CURVE('',#10327,#10329,#734,.T.);
#12651=EDGE_CURVE('',#10331,#10332,#6335,.T.);
#12652=EDGE_CURVE('',#10332,#10330,#735,.T.);
#12653=EDGE_CURVE('',#10329,#10331,#736,.T.);
#12654=EDGE_CURVE('',#10333,#10334,#6336,.T.);
#12655=EDGE_CURVE('',#10334,#10332,#737,.T.);
#12656=EDGE_CURVE('',#10331,#10333,#738,.T.);
#12657=EDGE_CURVE('',#10335,#10336,#6337,.T.);
#12658=EDGE_CURVE('',#10336,#10334,#739,.T.);
#12659=EDGE_CURVE('',#10333,#10335,#740,.T.);
#12660=EDGE_CURVE('',#10337,#10338,#6338,.T.);
#12661=EDGE_CURVE('',#10339,#10337,#9224,.F.);
#12662=EDGE_CURVE('',#10339,#10338,#741,.T.);
#12663=EDGE_CURVE('',#10340,#10341,#6339,.T.);
#12664=EDGE_CURVE('',#10341,#10342,#742,.T.);
#12665=EDGE_CURVE('',#10343,#10342,#9225,.T.);
#12666=EDGE_CURVE('',#10340,#10343,#743,.T.);
#12667=EDGE_CURVE('',#10344,#10345,#6340,.T.);
#12668=EDGE_CURVE('',#10345,#10341,#744,.T.);
#12669=EDGE_CURVE('',#10344,#10340,#745,.T.);
#12670=EDGE_CURVE('',#10346,#10347,#6341,.T.);
#12671=EDGE_CURVE('',#10347,#10345,#746,.T.);
#12672=EDGE_CURVE('',#10346,#10344,#747,.T.);
#12673=EDGE_CURVE('',#10348,#10349,#6342,.T.);
#12674=EDGE_CURVE('',#10349,#10347,#748,.T.);
#12675=EDGE_CURVE('',#10348,#10346,#749,.T.);
#12676=EDGE_CURVE('',#10350,#10351,#6343,.T.);
#12677=EDGE_CURVE('',#10351,#10349,#750,.T.);
#12678=EDGE_CURVE('',#10350,#10348,#751,.T.);
#12679=EDGE_CURVE('',#10352,#10353,#6344,.T.);
#12680=EDGE_CURVE('',#10353,#10351,#752,.T.);
#12681=EDGE_CURVE('',#10352,#10350,#753,.T.);
#12682=EDGE_CURVE('',#10354,#10355,#6345,.T.);
#12683=EDGE_CURVE('',#10355,#10353,#754,.T.);
#12684=EDGE_CURVE('',#10354,#10352,#755,.T.);
#12685=EDGE_CURVE('',#10356,#10357,#6346,.T.);
#12686=EDGE_CURVE('',#10357,#10355,#756,.T.);
#12687=EDGE_CURVE('',#10356,#10354,#757,.T.);
#12688=EDGE_CURVE('',#10358,#10359,#6347,.T.);
#12689=EDGE_CURVE('',#10360,#10358,#758,.T.);
#12690=EDGE_CURVE('',#10361,#10360,#9226,.T.);
#12691=EDGE_CURVE('',#10361,#10359,#759,.T.);
#12692=EDGE_CURVE('',#10359,#10357,#760,.T.);
#12693=EDGE_CURVE('',#10358,#10356,#761,.T.);
#12694=EDGE_CURVE('',#10342,#10339,#762,.T.);
#12695=EDGE_CURVE('',#10321,#10361,#763,.T.);
#12696=EDGE_CURVE('',#10338,#10336,#764,.T.);
#12697=EDGE_CURVE('',#10362,#10343,#765,.T.);
#12698=EDGE_CURVE('',#10335,#10362,#766,.T.);
#12699=EDGE_CURVE('',#10360,#10322,#767,.T.);
#12700=EDGE_CURVE('',#10363,#10364,#6348,.T.);
#12701=EDGE_CURVE('',#10364,#10363,#9227,.T.);
#12702=EDGE_CURVE('',#10337,#10362,#9228,.F.);
#12703=EDGE_CURVE('',#10365,#10365,#9229,.T.);
#12704=EDGE_CURVE('',#10366,#10366,#9230,.T.);
#12705=EDGE_CURVE('',#10367,#10367,#9231,.T.);
#12706=EDGE_CURVE('',#10368,#10368,#9232,.T.);
#12707=EDGE_CURVE('',#10368,#10367,#6349,.T.);
#12708=EDGE_CURVE('',#10369,#10369,#9233,.T.);
#12709=EDGE_CURVE('',#10369,#10366,#6350,.T.);
#12710=EDGE_CURVE('',#10370,#10370,#9234,.T.);
#12711=EDGE_CURVE('',#10370,#10365,#6351,.T.);
#12712=EDGE_CURVE('',#10371,#10372,#6352,.T.);
#12713=EDGE_CURVE('',#10364,#10371,#6353,.T.);
#12714=EDGE_CURVE('',#10372,#10363,#6354,.T.);
#12715=EDGE_CURVE('',#10371,#10372,#9235,.T.);
#12716=EDGE_CURVE('',#10373,#10373,#9236,.T.);
#12717=EDGE_CURVE('',#10373,#10374,#6355,.T.);
#12718=EDGE_CURVE('',#10374,#10374,#9237,.T.);
#16502=ORIENTED_EDGE('',*,*,#12635,.T.);
#16503=ORIENTED_EDGE('',*,*,#12636,.T.);
#16504=ORIENTED_EDGE('',*,*,#12637,.T.);
#16505=ORIENTED_EDGE('',*,*,#12638,.T.);
#16506=ORIENTED_EDGE('',*,*,#12639,.T.);
#16507=ORIENTED_EDGE('',*,*,#12640,.T.);
#16508=ORIENTED_EDGE('',*,*,#12635,.F.);
#16509=ORIENTED_EDGE('',*,*,#12641,.T.);
#16510=ORIENTED_EDGE('',*,*,#12642,.T.);
#16511=ORIENTED_EDGE('',*,*,#12643,.T.);
#16512=ORIENTED_EDGE('',*,*,#12639,.F.);
#16513=ORIENTED_EDGE('',*,*,#12644,.T.);
#16514=ORIENTED_EDGE('',*,*,#12645,.T.);
#16515=ORIENTED_EDGE('',*,*,#12646,.T.);
#16516=ORIENTED_EDGE('',*,*,#12642,.F.);
#16517=ORIENTED_EDGE('',*,*,#12647,.T.);
#16518=ORIENTED_EDGE('',*,*,#12648,.T.);
#16519=ORIENTED_EDGE('',*,*,#12649,.T.);
#16520=ORIENTED_EDGE('',*,*,#12645,.F.);
#16521=ORIENTED_EDGE('',*,*,#12650,.T.);
#16522=ORIENTED_EDGE('',*,*,#12651,.T.);
#16523=ORIENTED_EDGE('',*,*,#12652,.T.);
#16524=ORIENTED_EDGE('',*,*,#12648,.F.);
#16525=ORIENTED_EDGE('',*,*,#12653,.T.);
#16526=ORIENTED_EDGE('',*,*,#12654,.T.);
#16527=ORIENTED_EDGE('',*,*,#12655,.T.);
#16528=ORIENTED_EDGE('',*,*,#12651,.F.);
#16529=ORIENTED_EDGE('',*,*,#12656,.T.);
#16530=ORIENTED_EDGE('',*,*,#12657,.T.);
#16531=ORIENTED_EDGE('',*,*,#12658,.T.);
#16532=ORIENTED_EDGE('',*,*,#12654,.F.);
#16533=ORIENTED_EDGE('',*,*,#12659,.T.);
#16534=ORIENTED_EDGE('',*,*,#12660,.F.);
#16535=ORIENTED_EDGE('',*,*,#12661,.F.);
#16536=ORIENTED_EDGE('',*,*,#12662,.T.);
#16537=ORIENTED_EDGE('',*,*,#12663,.T.);
#16538=ORIENTED_EDGE('',*,*,#12664,.T.);
#16539=ORIENTED_EDGE('',*,*,#12665,.F.);
#16540=ORIENTED_EDGE('',*,*,#12666,.F.);
#16541=ORIENTED_EDGE('',*,*,#12667,.T.);
#16542=ORIENTED_EDGE('',*,*,#12668,.T.);
#16543=ORIENTED_EDGE('',*,*,#12663,.F.);
#16544=ORIENTED_EDGE('',*,*,#12669,.F.);
#16545=ORIENTED_EDGE('',*,*,#12670,.T.);
#16546=ORIENTED_EDGE('',*,*,#12671,.T.);
#16547=ORIENTED_EDGE('',*,*,#12667,.F.);
#16548=ORIENTED_EDGE('',*,*,#12672,.F.);
#16549=ORIENTED_EDGE('',*,*,#12673,.T.);
#16550=ORIENTED_EDGE('',*,*,#12674,.T.);
#16551=ORIENTED_EDGE('',*,*,#12670,.F.);
#16552=ORIENTED_EDGE('',*,*,#12675,.F.);
#16553=ORIENTED_EDGE('',*,*,#12676,.T.);
#16554=ORIENTED_EDGE('',*,*,#12677,.T.);
#16555=ORIENTED_EDGE('',*,*,#12673,.F.);
#16556=ORIENTED_EDGE('',*,*,#12678,.F.);
#16557=ORIENTED_EDGE('',*,*,#12679,.T.);
#16558=ORIENTED_EDGE('',*,*,#12680,.T.);
#16559=ORIENTED_EDGE('',*,*,#12676,.F.);
#16560=ORIENTED_EDGE('',*,*,#12681,.F.);
#16561=ORIENTED_EDGE('',*,*,#12682,.T.);
#16562=ORIENTED_EDGE('',*,*,#12683,.T.);
#16563=ORIENTED_EDGE('',*,*,#12679,.F.);
#16564=ORIENTED_EDGE('',*,*,#12684,.F.);
#16565=ORIENTED_EDGE('',*,*,#12685,.T.);
#16566=ORIENTED_EDGE('',*,*,#12686,.T.);
#16567=ORIENTED_EDGE('',*,*,#12682,.F.);
#16568=ORIENTED_EDGE('',*,*,#12687,.F.);
#16569=ORIENTED_EDGE('',*,*,#12688,.F.);
#16570=ORIENTED_EDGE('',*,*,#12689,.F.);
#16571=ORIENTED_EDGE('',*,*,#12690,.F.);
#16572=ORIENTED_EDGE('',*,*,#12691,.T.);
#16573=ORIENTED_EDGE('',*,*,#12688,.T.);
#16574=ORIENTED_EDGE('',*,*,#12692,.T.);
#16575=ORIENTED_EDGE('',*,*,#12685,.F.);
#16576=ORIENTED_EDGE('',*,*,#12693,.F.);
#16577=ORIENTED_EDGE('',*,*,#12694,.F.);
#16578=ORIENTED_EDGE('',*,*,#12664,.F.);
#16579=ORIENTED_EDGE('',*,*,#12668,.F.);
#16580=ORIENTED_EDGE('',*,*,#12671,.F.);
#16581=ORIENTED_EDGE('',*,*,#12674,.F.);
#16582=ORIENTED_EDGE('',*,*,#12677,.F.);
#16583=ORIENTED_EDGE('',*,*,#12680,.F.);
#16584=ORIENTED_EDGE('',*,*,#12683,.F.);
#16585=ORIENTED_EDGE('',*,*,#12686,.F.);
#16586=ORIENTED_EDGE('',*,*,#12692,.F.);
#16587=ORIENTED_EDGE('',*,*,#12691,.F.);
#16588=ORIENTED_EDGE('',*,*,#12695,.F.);
#16589=ORIENTED_EDGE('',*,*,#12636,.F.);
#16590=ORIENTED_EDGE('',*,*,#12640,.F.);
#16591=ORIENTED_EDGE('',*,*,#12643,.F.);
#16592=ORIENTED_EDGE('',*,*,#12646,.F.);
#16593=ORIENTED_EDGE('',*,*,#12649,.F.);
#16594=ORIENTED_EDGE('',*,*,#12652,.F.);
#16595=ORIENTED_EDGE('',*,*,#12655,.F.);
#16596=ORIENTED_EDGE('',*,*,#12658,.F.);
#16597=ORIENTED_EDGE('',*,*,#12696,.F.);
#16598=ORIENTED_EDGE('',*,*,#12662,.F.);
#16599=ORIENTED_EDGE('',*,*,#12697,.F.);
#16600=ORIENTED_EDGE('',*,*,#12698,.F.);
#16601=ORIENTED_EDGE('',*,*,#12659,.F.);
#16602=ORIENTED_EDGE('',*,*,#12656,.F.);
#16603=ORIENTED_EDGE('',*,*,#12653,.F.);
#16604=ORIENTED_EDGE('',*,*,#12650,.F.);
#16605=ORIENTED_EDGE('',*,*,#12647,.F.);
#16606=ORIENTED_EDGE('',*,*,#12644,.F.);
#16607=ORIENTED_EDGE('',*,*,#12641,.F.);
#16608=ORIENTED_EDGE('',*,*,#12638,.F.);
#16609=ORIENTED_EDGE('',*,*,#12699,.F.);
#16610=ORIENTED_EDGE('',*,*,#12689,.T.);
#16611=ORIENTED_EDGE('',*,*,#12693,.T.);
#16612=ORIENTED_EDGE('',*,*,#12687,.T.);
#16613=ORIENTED_EDGE('',*,*,#12684,.T.);
#16614=ORIENTED_EDGE('',*,*,#12681,.T.);
#16615=ORIENTED_EDGE('',*,*,#12678,.T.);
#16616=ORIENTED_EDGE('',*,*,#12675,.T.);
#16617=ORIENTED_EDGE('',*,*,#12672,.T.);
#16618=ORIENTED_EDGE('',*,*,#12669,.T.);
#16619=ORIENTED_EDGE('',*,*,#12666,.T.);
#16620=ORIENTED_EDGE('',*,*,#12700,.T.);
#16621=ORIENTED_EDGE('',*,*,#12701,.T.);
#16622=ORIENTED_EDGE('',*,*,#12697,.T.);
#16623=ORIENTED_EDGE('',*,*,#12665,.T.);
#16624=ORIENTED_EDGE('',*,*,#12694,.T.);
#16625=ORIENTED_EDGE('',*,*,#12661,.T.);
#16626=ORIENTED_EDGE('',*,*,#12702,.T.);
#16627=ORIENTED_EDGE('',*,*,#12703,.T.);
#16628=ORIENTED_EDGE('',*,*,#12704,.T.);
#16629=ORIENTED_EDGE('',*,*,#12705,.T.);
#16630=ORIENTED_EDGE('',*,*,#12706,.F.);
#16631=ORIENTED_EDGE('',*,*,#12707,.T.);
#16632=ORIENTED_EDGE('',*,*,#12705,.F.);
#16633=ORIENTED_EDGE('',*,*,#12707,.F.);
#16634=ORIENTED_EDGE('',*,*,#12708,.F.);
#16635=ORIENTED_EDGE('',*,*,#12709,.T.);
#16636=ORIENTED_EDGE('',*,*,#12704,.F.);
#16637=ORIENTED_EDGE('',*,*,#12709,.F.);
#16638=ORIENTED_EDGE('',*,*,#12710,.F.);
#16639=ORIENTED_EDGE('',*,*,#12711,.T.);
#16640=ORIENTED_EDGE('',*,*,#12703,.F.);
#16641=ORIENTED_EDGE('',*,*,#12711,.F.);
#16642=ORIENTED_EDGE('',*,*,#12712,.F.);
#16643=ORIENTED_EDGE('',*,*,#12713,.F.);
#16644=ORIENTED_EDGE('',*,*,#12700,.F.);
#16645=ORIENTED_EDGE('',*,*,#12714,.F.);
#16646=ORIENTED_EDGE('',*,*,#12712,.T.);
#16647=ORIENTED_EDGE('',*,*,#12715,.F.);
#16648=ORIENTED_EDGE('',*,*,#12706,.T.);
#16649=ORIENTED_EDGE('',*,*,#12708,.T.);
#16650=ORIENTED_EDGE('',*,*,#12710,.T.);
#16651=ORIENTED_EDGE('',*,*,#12716,.T.);
#16652=ORIENTED_EDGE('',*,*,#12714,.T.);
#16653=ORIENTED_EDGE('',*,*,#12701,.F.);
#16654=ORIENTED_EDGE('',*,*,#12713,.T.);
#16655=ORIENTED_EDGE('',*,*,#12715,.T.);
#16656=ORIENTED_EDGE('',*,*,#12660,.T.);
#16657=ORIENTED_EDGE('',*,*,#12696,.T.);
#16658=ORIENTED_EDGE('',*,*,#12657,.F.);
#16659=ORIENTED_EDGE('',*,*,#12698,.T.);
#16660=ORIENTED_EDGE('',*,*,#12702,.F.);
#16661=ORIENTED_EDGE('',*,*,#12716,.F.);
#16662=ORIENTED_EDGE('',*,*,#12717,.T.);
#16663=ORIENTED_EDGE('',*,*,#12718,.T.);
#16664=ORIENTED_EDGE('',*,*,#12717,.F.);
#16665=ORIENTED_EDGE('',*,*,#12718,.F.);
#16666=ORIENTED_EDGE('',*,*,#12699,.T.);
#16667=ORIENTED_EDGE('',*,*,#12637,.F.);
#16668=ORIENTED_EDGE('',*,*,#12695,.T.);
#16669=ORIENTED_EDGE('',*,*,#12690,.T.);
#21159=CYLINDRICAL_SURFACE('',#24753,0.457875);
#21160=CYLINDRICAL_SURFACE('',#24755,0.457875);
#21161=CYLINDRICAL_SURFACE('',#24756,0.457875);
#21162=CYLINDRICAL_SURFACE('',#24757,0.457875);
#21163=CYLINDRICAL_SURFACE('',#24758,0.457875);
#21164=CYLINDRICAL_SURFACE('',#24759,0.457875);
#21165=CYLINDRICAL_SURFACE('',#24760,0.457875);
#21166=CYLINDRICAL_SURFACE('',#24761,0.457875);
#21167=CYLINDRICAL_SURFACE('',#24762,0.457875);
#21168=CYLINDRICAL_SURFACE('',#24764,0.625);
#21169=CYLINDRICAL_SURFACE('',#24766,0.625);
#21170=CYLINDRICAL_SURFACE('',#24767,0.625);
#21171=CYLINDRICAL_SURFACE('',#24768,0.625);
#21172=CYLINDRICAL_SURFACE('',#24769,0.625);
#21173=CYLINDRICAL_SURFACE('',#24770,0.625);
#21174=CYLINDRICAL_SURFACE('',#24771,0.625);
#21175=CYLINDRICAL_SURFACE('',#24772,0.625);
#21176=CYLINDRICAL_SURFACE('',#24773,0.625);
#21177=CYLINDRICAL_SURFACE('',#24775,0.625);
#21178=CYLINDRICAL_SURFACE('',#24782,0.225);
#21179=CYLINDRICAL_SURFACE('',#24784,0.225);
#21180=CYLINDRICAL_SURFACE('',#24786,0.225);
#21181=CYLINDRICAL_SURFACE('',#24792,1.9);
#21182=CYLINDRICAL_SURFACE('',#24793,0.457875);
#21183=CYLINDRICAL_SURFACE('',#24794,1.1);
#22010=ADVANCED_FACE('',(#3229),#21159,.F.);
#22011=ADVANCED_FACE('',(#3230),#21160,.F.);
#22012=ADVANCED_FACE('',(#3231),#21161,.F.);
#22013=ADVANCED_FACE('',(#3232),#21162,.F.);
#22014=ADVANCED_FACE('',(#3233),#21163,.F.);
#22015=ADVANCED_FACE('',(#3234),#21164,.F.);
#22016=ADVANCED_FACE('',(#3235),#21165,.F.);
#22017=ADVANCED_FACE('',(#3236),#21166,.F.);
#22018=ADVANCED_FACE('',(#3237),#21167,.F.);
#22019=ADVANCED_FACE('',(#3238),#21168,.F.);
#22020=ADVANCED_FACE('',(#3239),#21169,.F.);
#22021=ADVANCED_FACE('',(#3240),#21170,.F.);
#22022=ADVANCED_FACE('',(#3241),#21171,.F.);
#22023=ADVANCED_FACE('',(#3242),#21172,.F.);
#22024=ADVANCED_FACE('',(#3243),#21173,.F.);
#22025=ADVANCED_FACE('',(#3244),#21174,.F.);
#22026=ADVANCED_FACE('',(#3245),#21175,.F.);
#22027=ADVANCED_FACE('',(#3246),#21176,.F.);
#22028=ADVANCED_FACE('',(#3247),#21177,.F.);
#22029=ADVANCED_FACE('',(#3248),#11,.F.);
#22030=ADVANCED_FACE('',(#3249),#12,.F.);
#22031=ADVANCED_FACE('',(#3250,#2050,#2051,#2052,#2053),#2491,.T.);
#22032=ADVANCED_FACE('',(#3251),#21178,.F.);
#22033=ADVANCED_FACE('',(#3252),#21179,.F.);
#22034=ADVANCED_FACE('',(#3253),#21180,.F.);
#22035=ADVANCED_FACE('',(#3254),#2492,.F.);
#22036=ADVANCED_FACE('',(#3255,#2054,#2055,#2056,#2057),#2493,.F.);
#22037=ADVANCED_FACE('',(#3256),#21181,.T.);
#22038=ADVANCED_FACE('',(#3257),#21182,.F.);
#22039=ADVANCED_FACE('',(#3258),#21183,.T.);
#22040=ADVANCED_FACE('',(#3259,#2058),#2494,.F.);
#23009=CLOSED_SHELL('',(#22010,#22011,#22012,#22013,#22014,#22015,#22016,
#22017,#22018,#22019,#22020,#22021,#22022,#22023,#22024,#22025,#22026,#22027,
#22028,#22029,#22030,#22031,#22032,#22033,#22034,#22035,#22036,#22037,#22038,
#22039,#22040));
#24752=AXIS2_PLACEMENT_3D('',#35256,#28389,#28390);
#24753=AXIS2_PLACEMENT_3D('',#35257,#28391,#28392);
#24754=AXIS2_PLACEMENT_3D('',#35288,#28394,#28395);
#24755=AXIS2_PLACEMENT_3D('',#35329,#28396,#28397);
#24756=AXIS2_PLACEMENT_3D('',#35416,#28399,#28400);
#24757=AXIS2_PLACEMENT_3D('',#35506,#28402,#28403);
#24758=AXIS2_PLACEMENT_3D('',#35593,#28405,#28406);
#24759=AXIS2_PLACEMENT_3D('',#35683,#28408,#28409);
#24760=AXIS2_PLACEMENT_3D('',#35770,#28411,#28412);
#24761=AXIS2_PLACEMENT_3D('',#35857,#28414,#28415);
#24762=AXIS2_PLACEMENT_3D('',#35947,#28417,#28418);
#24763=AXIS2_PLACEMENT_3D('',#35952,#28420,#28421);
#24764=AXIS2_PLACEMENT_3D('',#35963,#28422,#28423);
#24765=AXIS2_PLACEMENT_3D('',#35976,#28425,#28426);
#24766=AXIS2_PLACEMENT_3D('',#35989,#28427,#28428);
#24767=AXIS2_PLACEMENT_3D('',#36026,#28430,#28431);
#24768=AXIS2_PLACEMENT_3D('',#36063,#28433,#28434);
#24769=AXIS2_PLACEMENT_3D('',#36101,#28436,#28437);
#24770=AXIS2_PLACEMENT_3D('',#36138,#28439,#28440);
#24771=AXIS2_PLACEMENT_3D('',#36175,#28442,#28443);
#24772=AXIS2_PLACEMENT_3D('',#36213,#28445,#28446);
#24773=AXIS2_PLACEMENT_3D('',#36251,#28448,#28449);
#24774=AXIS2_PLACEMENT_3D('',#36262,#28451,#28452);
#24775=AXIS2_PLACEMENT_3D('',#36273,#28453,#28454);
#24776=AXIS2_PLACEMENT_3D('',#37416,#28455,#28456);
#24777=AXIS2_PLACEMENT_3D('',#37420,#28458,#28459);
#24778=AXIS2_PLACEMENT_3D('',#37421,#28460,#28461);
#24779=AXIS2_PLACEMENT_3D('',#37423,#28462,#28463);
#24780=AXIS2_PLACEMENT_3D('',#37425,#28464,#28465);
#24781=AXIS2_PLACEMENT_3D('',#37427,#28466,#28467);
#24782=AXIS2_PLACEMENT_3D('',#37428,#28468,#28469);
#24783=AXIS2_PLACEMENT_3D('',#37430,#28470,#28471);
#24784=AXIS2_PLACEMENT_3D('',#37432,#28473,#28474);
#24785=AXIS2_PLACEMENT_3D('',#37434,#28475,#28476);
#24786=AXIS2_PLACEMENT_3D('',#37436,#28478,#28479);
#24787=AXIS2_PLACEMENT_3D('',#37438,#28480,#28481);
#24788=AXIS2_PLACEMENT_3D('',#37440,#28483,#28484);
#24789=AXIS2_PLACEMENT_3D('',#37446,#28488,#28489);
#24790=AXIS2_PLACEMENT_3D('',#37447,#28490,#28491);
#24791=AXIS2_PLACEMENT_3D('',#37449,#28492,#28493);
#24792=AXIS2_PLACEMENT_3D('',#37450,#28494,#28495);
#24793=AXIS2_PLACEMENT_3D('',#37451,#28496,#28497);
#24794=AXIS2_PLACEMENT_3D('',#37452,#28498,#28499);
#24795=AXIS2_PLACEMENT_3D('',#37455,#28501,#28502);
#24796=AXIS2_PLACEMENT_3D('',#37456,#28503,#28504);
#28389=DIRECTION('axis',(0.,0.,1.));
#28390=DIRECTION('refdir',(1.,0.,0.));
#28391=DIRECTION('center_axis',(1.,0.,0.));
#28392=DIRECTION('ref_axis',(0.,0.207879895528894,-0.978154358490978));
#28393=DIRECTION('',(-1.,0.,0.));
#28394=DIRECTION('center_axis',(1.,0.,0.));
#28395=DIRECTION('ref_axis',(0.,0.,-1.));
#28396=DIRECTION('center_axis',(1.,0.,0.));
#28397=DIRECTION('ref_axis',(0.,0.,-1.));
#28398=DIRECTION('',(-1.,0.,0.));
#28399=DIRECTION('center_axis',(1.,0.,0.));
#28400=DIRECTION('ref_axis',(0.,0.,-1.));
#28401=DIRECTION('',(-1.,0.,0.));
#28402=DIRECTION('center_axis',(1.,0.,0.));
#28403=DIRECTION('ref_axis',(0.,0.,-1.));
#28404=DIRECTION('',(-1.,0.,0.));
#28405=DIRECTION('center_axis',(1.,0.,0.));
#28406=DIRECTION('ref_axis',(0.,0.,-1.));
#28407=DIRECTION('',(-1.,0.,0.));
#28408=DIRECTION('center_axis',(1.,0.,0.));
#28409=DIRECTION('ref_axis',(0.,0.,-1.));
#28410=DIRECTION('',(-1.,0.,0.));
#28411=DIRECTION('center_axis',(1.,0.,0.));
#28412=DIRECTION('ref_axis',(0.,0.,-1.));
#28413=DIRECTION('',(-1.,0.,0.));
#28414=DIRECTION('center_axis',(1.,0.,0.));
#28415=DIRECTION('ref_axis',(0.,0.,-1.));
#28416=DIRECTION('',(-1.,0.,0.));
#28417=DIRECTION('center_axis',(1.,0.,0.));
#28418=DIRECTION('ref_axis',(0.,0.,-1.));
#28419=DIRECTION('',(-1.,0.,0.));
#28420=DIRECTION('center_axis',(1.,0.,0.));
#28421=DIRECTION('ref_axis',(0.,0.,-1.));
#28422=DIRECTION('center_axis',(1.,0.,0.));
#28423=DIRECTION('ref_axis',(0.,2.68771689099506E-14,-1.));
#28424=DIRECTION('',(1.,3.30650148539799E-30,-1.22464679914735E-16));
#28425=DIRECTION('center_axis',(-1.,0.,0.));
#28426=DIRECTION('ref_axis',(0.,2.68771689099506E-14,-1.));
#28427=DIRECTION('center_axis',(1.,0.,0.));
#28428=DIRECTION('ref_axis',(0.,2.68771689099506E-14,-1.));
#28429=DIRECTION('',(1.,3.30650148539799E-30,-1.22464679914735E-16));
#28430=DIRECTION('center_axis',(1.,0.,0.));
#28431=DIRECTION('ref_axis',(0.,2.68771689099506E-14,-1.));
#28432=DIRECTION('',(1.,3.30650148539799E-30,-1.22464679914735E-16));
#28433=DIRECTION('center_axis',(1.,0.,0.));
#28434=DIRECTION('ref_axis',(0.,2.68771689099506E-14,-1.));
#28435=DIRECTION('',(1.,3.30650148539799E-30,-1.22464679914735E-16));
#28436=DIRECTION('center_axis',(1.,0.,0.));
#28437=DIRECTION('ref_axis',(0.,2.68771689099506E-14,-1.));
#28438=DIRECTION('',(1.,3.30650148539799E-30,-1.22464679914735E-16));
#28439=DIRECTION('center_axis',(1.,0.,0.));
#28440=DIRECTION('ref_axis',(0.,2.68771689099506E-14,-1.));
#28441=DIRECTION('',(1.,3.30650148539799E-30,-1.22464679914735E-16));
#28442=DIRECTION('center_axis',(1.,0.,0.));
#28443=DIRECTION('ref_axis',(0.,2.68771689099506E-14,-1.));
#28444=DIRECTION('',(1.,3.30650148539799E-30,-1.22464679914735E-16));
#28445=DIRECTION('center_axis',(1.,0.,0.));
#28446=DIRECTION('ref_axis',(0.,2.68771689099506E-14,-1.));
#28447=DIRECTION('',(1.,3.30650148539799E-30,-1.22464679914735E-16));
#28448=DIRECTION('center_axis',(1.,0.,0.));
#28449=DIRECTION('ref_axis',(0.,2.68771689099506E-14,-1.));
#28450=DIRECTION('',(1.,3.30650148539799E-30,-1.22464679914735E-16));
#28451=DIRECTION('center_axis',(1.,0.,0.));
#28452=DIRECTION('ref_axis',(0.,2.68771689099506E-14,-1.));
#28453=DIRECTION('center_axis',(1.,0.,0.));
#28454=DIRECTION('ref_axis',(0.,2.68771689099506E-14,-1.));
#28455=DIRECTION('center_axis',(1.,0.,0.));
#28456=DIRECTION('ref_axis',(0.,0.,-1.));
#28457=DIRECTION('',(0.,1.,0.));
#28458=DIRECTION('center_axis',(1.,0.,0.));
#28459=DIRECTION('ref_axis',(0.,0.,-1.));
#28460=DIRECTION('center_axis',(1.,0.,0.));
#28461=DIRECTION('ref_axis',(0.,0.,-1.));
#28462=DIRECTION('center_axis',(-1.,0.,0.));
#28463=DIRECTION('ref_axis',(0.,0.,-1.));
#28464=DIRECTION('center_axis',(-1.,0.,0.));
#28465=DIRECTION('ref_axis',(0.,0.,-1.));
#28466=DIRECTION('center_axis',(-1.,0.,0.));
#28467=DIRECTION('ref_axis',(0.,0.,-1.));
#28468=DIRECTION('center_axis',(1.,0.,0.));
#28469=DIRECTION('ref_axis',(0.,0.,-1.));
#28470=DIRECTION('center_axis',(1.,0.,0.));
#28471=DIRECTION('ref_axis',(0.,0.,-1.));
#28472=DIRECTION('',(1.,0.,0.));
#28473=DIRECTION('center_axis',(1.,0.,0.));
#28474=DIRECTION('ref_axis',(0.,0.,-1.));
#28475=DIRECTION('center_axis',(1.,0.,0.));
#28476=DIRECTION('ref_axis',(0.,0.,-1.));
#28477=DIRECTION('',(1.,0.,0.));
#28478=DIRECTION('center_axis',(1.,0.,0.));
#28479=DIRECTION('ref_axis',(0.,0.,-1.));
#28480=DIRECTION('center_axis',(1.,0.,0.));
#28481=DIRECTION('ref_axis',(0.,0.,-1.));
#28482=DIRECTION('',(1.,0.,0.));
#28483=DIRECTION('center_axis',(0.,0.,1.));
#28484=DIRECTION('ref_axis',(0.,-1.,0.));
#28485=DIRECTION('',(0.,-1.,0.));
#28486=DIRECTION('',(-1.,0.,0.));
#28487=DIRECTION('',(1.,0.,0.));
#28488=DIRECTION('center_axis',(1.,0.,0.));
#28489=DIRECTION('ref_axis',(0.,0.,-1.));
#28490=DIRECTION('center_axis',(1.,0.,0.));
#28491=DIRECTION('ref_axis',(0.,0.,-1.));
#28492=DIRECTION('center_axis',(1.,0.,0.));
#28493=DIRECTION('ref_axis',(0.,0.,-1.));
#28494=DIRECTION('center_axis',(1.,0.,0.));
#28495=DIRECTION('ref_axis',(0.,-1.22464679914735E-16,1.));
#28496=DIRECTION('center_axis',(1.,0.,0.));
#28497=DIRECTION('ref_axis',(0.,0.,-1.));
#28498=DIRECTION('center_axis',(1.,0.,0.));
#28499=DIRECTION('ref_axis',(0.,0.,-1.));
#28500=DIRECTION('',(-1.,0.,0.));
#28501=DIRECTION('center_axis',(1.,0.,0.));
#28502=DIRECTION('ref_axis',(0.,0.,-1.));
#28503=DIRECTION('center_axis',(1.,0.,0.));
#28504=DIRECTION('ref_axis',(0.,0.,-1.));
#35256=CARTESIAN_POINT('',(0.,0.,0.));
#35257=CARTESIAN_POINT('Origin',(12.5,0.,4.));
#35258=CARTESIAN_POINT('',(12.7800042915148,-1.13874042544416E-5,4.45787212683272));
#35259=CARTESIAN_POINT('',(12.6699957084852,1.09516003635735E-5,4.45788309353564));
#35260=CARTESIAN_POINT('',(12.5,-5.60735153159594E-17,4.457875));
#35261=CARTESIAN_POINT('',(12.5,-0.186196943290586,3.58169363627331));
#35262=CARTESIAN_POINT('Ctrl Pts',(12.6699957084852,1.09516003635735E-5,
4.45788309353564));
#35263=CARTESIAN_POINT('Ctrl Pts',(12.6684300766731,0.0150239422001319,
4.45789815019349));
#35264=CARTESIAN_POINT('Ctrl Pts',(12.6668644448611,0.0300354905662504,
4.45717403092565));
#35265=CARTESIAN_POINT('Ctrl Pts',(12.6652988130491,0.0449730203321769,
4.45569984746698));
#35266=CARTESIAN_POINT('Ctrl Pts',(12.6574274409991,0.120072959788606,4.44828824124903));
#35267=CARTESIAN_POINT('Ctrl Pts',(12.6495560689492,0.193301947984492,4.42191743369942));
#35268=CARTESIAN_POINT('Ctrl Pts',(12.6416846968992,0.255884660534875,4.37974732787395));
#35269=CARTESIAN_POINT('Ctrl Pts',(12.6338133248492,0.318467373085258,4.33757722204849));
#35270=CARTESIAN_POINT('Ctrl Pts',(12.6259419527993,0.370403809990138,4.27960781794716));
#35271=CARTESIAN_POINT('Ctrl Pts',(12.6180705807493,0.405471379329245,4.2127856577826));
#35272=CARTESIAN_POINT('Ctrl Pts',(12.6101992086994,0.440538948668352,4.14596349761803));
#35273=CARTESIAN_POINT('Ctrl Pts',(12.6023278366494,0.458737650441686,4.07028858139023));
#35274=CARTESIAN_POINT('Ctrl Pts',(12.5944564645995,0.457884906392306,3.99482861029462));
#35275=CARTESIAN_POINT('Ctrl Pts',(12.5865850925495,0.457032162342926,3.91936863919901));
#35276=CARTESIAN_POINT('Ctrl Pts',(12.5787137204996,0.437127972470831,3.84412361323559));
#35277=CARTESIAN_POINT('Ctrl Pts',(12.5708423484496,0.400561475243013,3.77811083326841));
#35278=CARTESIAN_POINT('Ctrl Pts',(12.5629709763996,0.363994978015195,3.71209805330123));
#35279=CARTESIAN_POINT('Ctrl Pts',(12.5550996043497,0.310766173431653,3.6553175193303));
#35280=CARTESIAN_POINT('Ctrl Pts',(12.5472282322997,0.247245050961511,3.61457214242492));
#35281=CARTESIAN_POINT('Ctrl Pts',(12.5393568602498,0.183723928491369,3.57382676551955));
#35282=CARTESIAN_POINT('Ctrl Pts',(12.5314854881998,0.109910488134627,3.54911654567973));
#35283=CARTESIAN_POINT('Ctrl Pts',(12.5236141161499,0.034670519197381,3.5434092666393));
#35284=CARTESIAN_POINT('Ctrl Pts',(12.5157427440999,-0.0405694497398647,
3.53770198759887));
#35285=CARTESIAN_POINT('Ctrl Pts',(12.50787137205,-0.117235947257613,3.55099764935784));
#35286=CARTESIAN_POINT('Ctrl Pts',(12.5,-0.186196943290592,3.58169363627332));
#35287=CARTESIAN_POINT('',(12.5,-0.186217277007329,4.41832740439831));
#35288=CARTESIAN_POINT('Origin',(12.5,0.,4.));
#35289=CARTESIAN_POINT('Ctrl Pts',(12.5,-0.186217277007329,4.41832740439831));
#35290=CARTESIAN_POINT('Ctrl Pts',(12.5008157411716,-0.193365324225124,
4.41515241707318));
#35291=CARTESIAN_POINT('Ctrl Pts',(12.5016314823431,-0.200430783441492,
4.4117927098014));
#35292=CARTESIAN_POINT('Ctrl Pts',(12.5024472235147,-0.207403505574881,
4.40825058102053));
#35293=CARTESIAN_POINT('Ctrl Pts',(12.5103185955646,-0.274685741688951,
4.37407134077235));
#35294=CARTESIAN_POINT('Ctrl Pts',(12.5181899676146,-0.333333232193243,
4.32290684204764));
#35295=CARTESIAN_POINT('Ctrl Pts',(12.5260613396645,-0.376326743005614,
4.26088786252735));
#35296=CARTESIAN_POINT('Ctrl Pts',(12.5339327117145,-0.419320253817985,
4.19886888300706));
#35297=CARTESIAN_POINT('Ctrl Pts',(12.5418040837645,-0.446659784938435,
4.12599542269119));
#35298=CARTESIAN_POINT('Ctrl Pts',(12.5496754558144,-0.455065168373522,
4.05100019606997));
#35299=CARTESIAN_POINT('Ctrl Pts',(12.5575468278644,-0.463470551808608,
3.97600496944875));
#35300=CARTESIAN_POINT('Ctrl Pts',(12.5654181999143,-0.452941787558331,
3.89888797652218));
#35301=CARTESIAN_POINT('Ctrl Pts',(12.5732895719643,-0.424742400952558,
3.82888990513641));
#35302=CARTESIAN_POINT('Ctrl Pts',(12.5811609440142,-0.396543014346786,
3.75889183375065));
#35303=CARTESIAN_POINT('Ctrl Pts',(12.5890323160642,-0.350673005385519,
3.69601268390568));
#35304=CARTESIAN_POINT('Ctrl Pts',(12.5969036881141,-0.292628022669152,
3.64778723809593));
#35305=CARTESIAN_POINT('Ctrl Pts',(12.6047750601641,-0.234583039952784,
3.59956179228618));
#35306=CARTESIAN_POINT('Ctrl Pts',(12.6126464322141,-0.164363083481316,
3.56599005051166));
#35307=CARTESIAN_POINT('Ctrl Pts',(12.620517804264,-0.0903829156297007,
3.55109483330951));
#35308=CARTESIAN_POINT('Ctrl Pts',(12.628389176314,-0.0164027477780855,
3.53619961610736));
#35309=CARTESIAN_POINT('Ctrl Pts',(12.6362605483639,0.0613376314536766,
3.53998092347757));
#35310=CARTESIAN_POINT('Ctrl Pts',(12.6441319204139,0.13352290298843,3.56198566164487));
#35311=CARTESIAN_POINT('Ctrl Pts',(12.6520032924638,0.205708174523184,3.58399039981218));
#35312=CARTESIAN_POINT('Ctrl Pts',(12.6598746645138,0.272338338360929,3.62421856877658));
#35313=CARTESIAN_POINT('Ctrl Pts',(12.6677460365637,0.325429113408527,3.67784968145944));
#35314=CARTESIAN_POINT('Ctrl Pts',(12.6756174086137,0.378519888456125,3.7314807941423));
#35315=CARTESIAN_POINT('Ctrl Pts',(12.6834887806637,0.418071274713577,3.79851485054363));
#35316=CARTESIAN_POINT('Ctrl Pts',(12.6913601527136,0.439343931585728,3.87091926467948));
#35317=CARTESIAN_POINT('Ctrl Pts',(12.6992315247636,0.460616588457879,3.94332367881533));
#35318=CARTESIAN_POINT('Ctrl Pts',(12.7071028968135,0.46361051594473,4.02109845068571));
#35319=CARTESIAN_POINT('Ctrl Pts',(12.7149742688635,0.447966936692366,4.09492394607626));
#35320=CARTESIAN_POINT('Ctrl Pts',(12.7228456409134,0.432323357440003,4.16874944146681));
#35321=CARTESIAN_POINT('Ctrl Pts',(12.7307170129634,0.398042271448426,4.23862566037754));
#35322=CARTESIAN_POINT('Ctrl Pts',(12.7385883850133,0.349231538304918,4.29617944234672));
#35323=CARTESIAN_POINT('Ctrl Pts',(12.7464597570633,0.300420805161409,4.35373322431589));
#35324=CARTESIAN_POINT('Ctrl Pts',(12.7543311291133,0.237080424865968,4.39896456934351));
#35325=CARTESIAN_POINT('Ctrl Pts',(12.7622025011632,0.166800374688878,4.42645347375649));
#35326=CARTESIAN_POINT('Ctrl Pts',(12.7681364312804,0.113818899065861,4.4471763206439));
#35327=CARTESIAN_POINT('Ctrl Pts',(12.7740703613976,0.056893551674301,4.45781599184163));
#35328=CARTESIAN_POINT('Ctrl Pts',(12.7800042915148,-1.13874042544416E-5,
4.45787212683272));
#35329=CARTESIAN_POINT('Origin',(12.5,0.,4.));
#35330=CARTESIAN_POINT('',(13.0800042915148,2.8196954984682E-6,4.45783894202495));
#35331=CARTESIAN_POINT('',(12.9699957084852,-6.90274666573233E-6,4.45790451736119));
#35332=CARTESIAN_POINT('',(12.5,-5.60735153159594E-17,4.457875));
#35333=CARTESIAN_POINT('Ctrl Pts',(12.9699957084852,-6.90274666573233E-6,
4.45790451736119));
#35334=CARTESIAN_POINT('Ctrl Pts',(12.9628865412726,0.0681543496286777,
4.45785453236543));
#35335=CARTESIAN_POINT('Ctrl Pts',(12.95577737406,0.136337475731944,4.44242789501186));
#35336=CARTESIAN_POINT('Ctrl Pts',(12.9486682068475,0.197807532932104,4.41298560914613));
#35337=CARTESIAN_POINT('Ctrl Pts',(12.9407968347975,0.265868063186489,4.38038668734267));
#35338=CARTESIAN_POINT('Ctrl Pts',(12.9329254627476,0.325698883531032,4.33060565060516));
#35339=CARTESIAN_POINT('Ctrl Pts',(12.9250540906976,0.370130557623211,4.26960768492436));
#35340=CARTESIAN_POINT('Ctrl Pts',(12.9171827186476,0.41456223171539,4.20860971924356));
#35341=CARTESIAN_POINT('Ctrl Pts',(12.9093113465977,0.443594759555206,4.13639482461947));
#35342=CARTESIAN_POINT('Ctrl Pts',(12.9014399745477,0.453749217534713,4.06161640217293));
#35343=CARTESIAN_POINT('Ctrl Pts',(12.8935686024978,0.463903675514219,3.9868379797264));
#35344=CARTESIAN_POINT('Ctrl Pts',(12.8856972304478,0.455180063633418,3.90949602945742));
#35345=CARTESIAN_POINT('Ctrl Pts',(12.8778258583979,0.428623718850503,3.83885831972366));
#35346=CARTESIAN_POINT('Ctrl Pts',(12.8699544863479,0.402067374067587,3.7682206099899));
#35347=CARTESIAN_POINT('Ctrl Pts',(12.862083114298,0.357678296382559,3.70428714079136));
#35348=CARTESIAN_POINT('Ctrl Pts',(12.854211742248,0.300775561959983,3.65471896268111));
#35349=CARTESIAN_POINT('Ctrl Pts',(12.846340370198,0.243872827537407,3.60515078457087));
#35350=CARTESIAN_POINT('Ctrl Pts',(12.8384689981481,0.174456436377283,3.56994789754891));
#35351=CARTESIAN_POINT('Ctrl Pts',(12.8305976260981,0.100844448250471,3.55332860992135));
#35352=CARTESIAN_POINT('Ctrl Pts',(12.8227262540482,0.0272324601236582,
3.53670932229378));
#35353=CARTESIAN_POINT('Ctrl Pts',(12.8148548819982,-0.0505751249698428,
3.53867363406062));
#35354=CARTESIAN_POINT('Ctrl Pts',(12.8069835099483,-0.123254740362562,
3.558986165072));
#35355=CARTESIAN_POINT('Ctrl Pts',(12.7991121378983,-0.195934355755281,
3.57929869608338));
#35356=CARTESIAN_POINT('Ctrl Pts',(12.7912407658484,-0.263486001447217,
3.6179594463393));
#35357=CARTESIAN_POINT('Ctrl Pts',(12.7833693937984,-0.317815070570116,
3.67033575613656));
#35358=CARTESIAN_POINT('Ctrl Pts',(12.7754980217484,-0.372144139693014,
3.72271206593382));
#35359=CARTESIAN_POINT('Ctrl Pts',(12.7676266496985,-0.413250632246875,
3.78880393527241));
#35360=CARTESIAN_POINT('Ctrl Pts',(12.7597552776485,-0.43620881068128,3.86069167744737));
#35361=CARTESIAN_POINT('Ctrl Pts',(12.7518839055986,-0.459166989115684,
3.93257941962233));
#35362=CARTESIAN_POINT('Ctrl Pts',(12.7440125335486,-0.463976853430633,
4.01026303463365));
#35363=CARTESIAN_POINT('Ctrl Pts',(12.7361411614987,-0.450062064178823,
4.08443380953254));
#35364=CARTESIAN_POINT('Ctrl Pts',(12.7282697894487,-0.436147274927012,
4.15860458443143));
#35365=CARTESIAN_POINT('Ctrl Pts',(12.7203984173988,-0.403507832108441,
4.22926251921788));
#35366=CARTESIAN_POINT('Ctrl Pts',(12.7125270453488,-0.356054829243877,
4.28794078818664));
#35367=CARTESIAN_POINT('Ctrl Pts',(12.7046556732988,-0.308601826379312,
4.3466190571554));
#35368=CARTESIAN_POINT('Ctrl Pts',(12.6967843012489,-0.246335263468753,
4.39331766030646));
#35369=CARTESIAN_POINT('Ctrl Pts',(12.6889129291989,-0.176716536654988,
4.42244075943884));
#35370=CARTESIAN_POINT('Ctrl Pts',(12.682607188961,-0.120945115332726,4.44577121528397));
#35371=CARTESIAN_POINT('Ctrl Pts',(12.6763014487231,-0.0604553842193124,
4.45782245132557));
#35372=CARTESIAN_POINT('Ctrl Pts',(12.6699957084852,1.09516003635735E-5,
4.45788309353564));
#35373=CARTESIAN_POINT('Ctrl Pts',(12.7800042915148,-1.13874042544416E-5,
4.45787212683272));
#35374=CARTESIAN_POINT('Ctrl Pts',(12.7819417334476,-0.0185909818676029,
4.45789045503738));
#35375=CARTESIAN_POINT('Ctrl Pts',(12.7838791753803,-0.0371684007279871,
4.45678053845584));
#35376=CARTESIAN_POINT('Ctrl Pts',(12.7858166173131,-0.0556056617636943,
4.45452496135198));
#35377=CARTESIAN_POINT('Ctrl Pts',(12.793687989363,-0.130511927980435,4.44536108073615));
#35378=CARTESIAN_POINT('Ctrl Pts',(12.801559361413,-0.203104740355178,4.41728685570614));
#35379=CARTESIAN_POINT('Ctrl Pts',(12.8094307334629,-0.264685413403174,
4.37366637792357));
#35380=CARTESIAN_POINT('Ctrl Pts',(12.8173021055129,-0.32626608645117,4.33004590014099));
#35381=CARTESIAN_POINT('Ctrl Pts',(12.8251734775629,-0.37683462017242,4.27087916960585));
#35382=CARTESIAN_POINT('Ctrl Pts',(12.8330448496128,-0.410331463567461,
4.20325604577686));
#35383=CARTESIAN_POINT('Ctrl Pts',(12.8409162216628,-0.443828306962503,
4.13563292194788));
#35384=CARTESIAN_POINT('Ctrl Pts',(12.8487875937127,-0.460253460031337,
4.05955340482505));
#35385=CARTESIAN_POINT('Ctrl Pts',(12.8566589657627,-0.457638721839564,
3.98413398734005));
#35386=CARTESIAN_POINT('Ctrl Pts',(12.8645303378126,-0.45502398364779,3.90871456985506));
#35387=CARTESIAN_POINT('Ctrl Pts',(12.8724017098626,-0.433369354195409,
3.8339552520079));
#35388=CARTESIAN_POINT('Ctrl Pts',(12.8802730819125,-0.395269674734573,
3.76881432927916));
#35389=CARTESIAN_POINT('Ctrl Pts',(12.8881444539625,-0.357169995273737,
3.70367340655041));
#35390=CARTESIAN_POINT('Ctrl Pts',(12.8960158260125,-0.302625265804445,
3.64815087894007));
#35391=CARTESIAN_POINT('Ctrl Pts',(12.9038871980624,-0.238171498431664,
3.6088999265713));
#35392=CARTESIAN_POINT('Ctrl Pts',(12.9117585701124,-0.173717731058884,
3.56964897420252));
#35393=CARTESIAN_POINT('Ctrl Pts',(12.9196299421623,-0.0993549257826154,
3.5466695970753));
#35394=CARTESIAN_POINT('Ctrl Pts',(12.9275013142123,-0.023993864556795,
3.54271537903906));
#35395=CARTESIAN_POINT('Ctrl Pts',(12.9353726862622,0.0513671966690251,
3.53876116100282));
#35396=CARTESIAN_POINT('Ctrl Pts',(12.9432440583122,0.127726513844396,3.55383210205756));
#35397=CARTESIAN_POINT('Ctrl Pts',(12.9511154303621,0.195934065997641,3.58612227423372));
#35398=CARTESIAN_POINT('Ctrl Pts',(12.9589868024121,0.264141618150887,3.61841244640988));
#35399=CARTESIAN_POINT('Ctrl Pts',(12.9668581744621,0.324197405282005,3.66792184970745));
#35400=CARTESIAN_POINT('Ctrl Pts',(12.974729546512,0.368905033668178,3.72871784755079));
#35401=CARTESIAN_POINT('Ctrl Pts',(12.982600918562,0.41361266205435,3.78951384539413));
#35402=CARTESIAN_POINT('Ctrl Pts',(12.9904722906119,0.442972131695578,3.86159643778324));
#35403=CARTESIAN_POINT('Ctrl Pts',(12.9983436626619,0.453465341949404,3.93632807718928));
#35404=CARTESIAN_POINT('Ctrl Pts',(13.0062150347118,0.46395855220323,4.01105971659532));
#35405=CARTESIAN_POINT('Ctrl Pts',(13.0140864067618,0.455585503069655,4.0884404030183));
#35406=CARTESIAN_POINT('Ctrl Pts',(13.0219577788117,0.429349524305901,4.15919772637108));
#35407=CARTESIAN_POINT('Ctrl Pts',(13.0298291508617,0.403113545542148,4.22995504972387));
#35408=CARTESIAN_POINT('Ctrl Pts',(13.0377005229117,0.359014637148215,4.29408901000646));
#35409=CARTESIAN_POINT('Ctrl Pts',(13.0455718949616,0.302337104315659,4.34391453219887));
#35410=CARTESIAN_POINT('Ctrl Pts',(13.0534432670116,0.245659571483104,4.39374005439127));
#35411=CARTESIAN_POINT('Ctrl Pts',(13.0613146390615,0.176403414211925,4.4292571384935));
#35412=CARTESIAN_POINT('Ctrl Pts',(13.0691860111115,0.102867492605122,4.44620982627979));
#35413=CARTESIAN_POINT('Ctrl Pts',(13.0727921045793,0.0691786509558273,
4.45397632191734));
#35414=CARTESIAN_POINT('Ctrl Pts',(13.076398198047,0.0345915681853763,4.45784650391406));
#35415=CARTESIAN_POINT('Ctrl Pts',(13.0800042915148,2.8196954984682E-6,
4.45783894202495));
#35416=CARTESIAN_POINT('Origin',(12.5,0.,4.));
#35417=CARTESIAN_POINT('',(13.3800042915148,1.00338821889499E-5,4.45789143379912));
#35418=CARTESIAN_POINT('',(13.2699957084852,-6.83105689078257E-6,4.45784477598907));
#35419=CARTESIAN_POINT('',(12.5,-5.60735153159594E-17,4.457875));
#35420=CARTESIAN_POINT('Ctrl Pts',(13.2699957084852,-6.83105689078257E-6,
4.45784477598907));
#35421=CARTESIAN_POINT('Ctrl Pts',(13.265214377922,0.0458528260712244,4.45782008288951));
#35422=CARTESIAN_POINT('Ctrl Pts',(13.2604330473589,0.091719698604501,4.45096974854549));
#35423=CARTESIAN_POINT('Ctrl Pts',(13.2556517167957,0.135506404234727,4.43740478719402));
#35424=CARTESIAN_POINT('Ctrl Pts',(13.2477803447458,0.207591244700251,4.41507316710824));
#35425=CARTESIAN_POINT('Ctrl Pts',(13.2399089726958,0.274038390871736,4.37454348113122));
#35426=CARTESIAN_POINT('Ctrl Pts',(13.2320376006459,0.326885582178656,4.32067233995558));
#35427=CARTESIAN_POINT('Ctrl Pts',(13.2241662285959,0.379732773485576,4.26680119877995));
#35428=CARTESIAN_POINT('Ctrl Pts',(13.2162948565459,0.418980009927931,4.19958860240569));
#35429=CARTESIAN_POINT('Ctrl Pts',(13.208423484496,0.439924354792367,4.12708853413817));
#35430=CARTESIAN_POINT('Ctrl Pts',(13.200552112446,0.460868699656804,4.05458846587065));
#35431=CARTESIAN_POINT('Ctrl Pts',(13.1926807403961,0.463510152943321,3.97680092570987));
#35432=CARTESIAN_POINT('Ctrl Pts',(13.1848093683461,0.447532193317848,3.90304707640827));
#35433=CARTESIAN_POINT('Ctrl Pts',(13.1769379962962,0.431554233692375,3.82929322710668));
#35434=CARTESIAN_POINT('Ctrl Pts',(13.1690666242462,0.396956861154912,3.75957306866428));
#35435=CARTESIAN_POINT('Ctrl Pts',(13.1611952521963,0.347885826291745,3.70224106173923));
#35436=CARTESIAN_POINT('Ctrl Pts',(13.1533238801463,0.298814791428577,3.64490905481418));
#35437=CARTESIAN_POINT('Ctrl Pts',(13.1454525080963,0.235270094239705,3.59996519940648));
#35438=CARTESIAN_POINT('Ctrl Pts',(13.1375811360464,0.164866199243897,3.57279504942506));
#35439=CARTESIAN_POINT('Ctrl Pts',(13.1297097639964,0.0944623042480882,
3.54562489944363));
#35440=CARTESIAN_POINT('Ctrl Pts',(13.1218383919465,0.0171992114453437,
3.53622845488849));
#35441=CARTESIAN_POINT('Ctrl Pts',(13.1139670198965,-0.0576647601420857,
3.54573167743434));
#35442=CARTESIAN_POINT('Ctrl Pts',(13.1060956478466,-0.132528731729515,
3.55523489998019));
#35443=CARTESIAN_POINT('Ctrl Pts',(13.0982242757966,-0.204993582101629,
3.58363778962703));
#35444=CARTESIAN_POINT('Ctrl Pts',(13.0903529037467,-0.266375958336211,
3.62753687126191));
#35445=CARTESIAN_POINT('Ctrl Pts',(13.0824815316967,-0.327758334570793,
3.67143595289679));
#35446=CARTESIAN_POINT('Ctrl Pts',(13.0746101596467,-0.378058236667844,
3.73083122651971));
#35447=CARTESIAN_POINT('Ctrl Pts',(13.0667387875968,-0.411248303781717,
3.79860544673343));
#35448=CARTESIAN_POINT('Ctrl Pts',(13.0588674155468,-0.444438370895591,
3.86637966694714));
#35449=CARTESIAN_POINT('Ctrl Pts',(13.0509960434969,-0.460518603026287,
3.94253283375165));
#35450=CARTESIAN_POINT('Ctrl Pts',(13.0431246714469,-0.457562130387816,
4.0179396288708));
#35451=CARTESIAN_POINT('Ctrl Pts',(13.035253299397,-0.454605657749345,4.09334642398995));
#35452=CARTESIAN_POINT('Ctrl Pts',(13.027381927347,-0.432612480341706,4.16800684742375));
#35453=CARTESIAN_POINT('Ctrl Pts',(13.0195105552971,-0.394218007200806,
4.23297445406563));
#35454=CARTESIAN_POINT('Ctrl Pts',(13.0116391832471,-0.355823534059905,
4.29794206070751));
#35455=CARTESIAN_POINT('Ctrl Pts',(13.0037678111972,-0.301027765185743,
4.35321685055749));
#35456=CARTESIAN_POINT('Ctrl Pts',(12.9958964391472,-0.236396794305188,
4.39217532952931));
#35457=CARTESIAN_POINT('Ctrl Pts',(12.9880250670972,-0.171765823424632,
4.43113380850113));
#35458=CARTESIAN_POINT('Ctrl Pts',(12.9801536950473,-0.0972996505376846,
4.45377597659478));
#35459=CARTESIAN_POINT('Ctrl Pts',(12.9722823229973,-0.0219214440120968,
4.4573886572069));
#35460=CARTESIAN_POINT('Ctrl Pts',(12.9715201181599,-0.014622381881285,
4.45773848219561));
#35461=CARTESIAN_POINT('Ctrl Pts',(12.9707579133226,-0.00731476803234869,
4.45790987647069));
#35462=CARTESIAN_POINT('Ctrl Pts',(12.9699957084852,-6.90274666573233E-6,
4.45790451736119));
#35463=CARTESIAN_POINT('Ctrl Pts',(13.0800042915148,2.8196954984682E-6,
4.45783894202495));
#35464=CARTESIAN_POINT('Ctrl Pts',(13.084269570097,-0.0409086678841046,
4.4578299978409));
#35465=CARTESIAN_POINT('Ctrl Pts',(13.0885348486792,-0.0818224858219862,
4.45239605085009));
#35466=CARTESIAN_POINT('Ctrl Pts',(13.0928001272613,-0.121255029803553,
4.44156782927524));
#35467=CARTESIAN_POINT('Ctrl Pts',(13.1006714993113,-0.194025944662995,
4.42158485301405));
#35468=CARTESIAN_POINT('Ctrl Pts',(13.1085428713613,-0.261752088439453,
4.3832306090213));
#35469=CARTESIAN_POINT('Ctrl Pts',(13.1164142434112,-0.31631794022257,4.33110102808186));
#35470=CARTESIAN_POINT('Ctrl Pts',(13.1242856154612,-0.370883792005687,
4.27897144714243));
#35471=CARTESIAN_POINT('Ctrl Pts',(13.1321569875111,-0.412289351795463,
4.21306652925631));
#35472=CARTESIAN_POINT('Ctrl Pts',(13.1400283595611,-0.435573054271055,
4.14128356060242));
#35473=CARTESIAN_POINT('Ctrl Pts',(13.147899731611,-0.458856756746647,4.06950059194853));
#35474=CARTESIAN_POINT('Ctrl Pts',(13.155771103661,-0.464018601908056,3.99183957252686));
#35475=CARTESIAN_POINT('Ctrl Pts',(13.1636424757109,-0.45044005369213,3.91760650430194));
#35476=CARTESIAN_POINT('Ctrl Pts',(13.1715138477609,-0.436861505476204,
3.84337343607703));
#35477=CARTESIAN_POINT('Ctrl Pts',(13.1793852198109,-0.404542563882944,
3.77256831904885));
#35478=CARTESIAN_POINT('Ctrl Pts',(13.1872565918608,-0.357355958580309,
3.7136756228145));
#35479=CARTESIAN_POINT('Ctrl Pts',(13.1951279639108,-0.310169353277673,
3.65478292658016));
#35480=CARTESIAN_POINT('Ctrl Pts',(13.2029993359607,-0.248115084265664,
3.60780265113964));
#35481=CARTESIAN_POINT('Ctrl Pts',(13.2108707080107,-0.178629020319019,
3.57836437152041));
#35482=CARTESIAN_POINT('Ctrl Pts',(13.2187420800606,-0.109142956372374,
3.54892609190117));
#35483=CARTESIAN_POINT('Ctrl Pts',(13.2266134521106,-0.0322250974910928,
3.53702980810322));
#35484=CARTESIAN_POINT('Ctrl Pts',(13.2344848241605,0.0429076061587562,
3.54410103373967));
#35485=CARTESIAN_POINT('Ctrl Pts',(13.2423561962105,0.118040309808605,3.55117225937612));
#35486=CARTESIAN_POINT('Ctrl Pts',(13.2502275682605,0.191387858227023,3.57721099444696));
#35487=CARTESIAN_POINT('Ctrl Pts',(13.2580989403104,0.254161126126225,3.61909705689013));
#35488=CARTESIAN_POINT('Ctrl Pts',(13.2659703123604,0.316934394025428,3.66098311933329));
#35489=CARTESIAN_POINT('Ctrl Pts',(13.2738416844103,0.369133381405416,3.71871650914877));
#35490=CARTESIAN_POINT('Ctrl Pts',(13.2817130564603,0.404503162915977,3.78537912195109));
#35491=CARTESIAN_POINT('Ctrl Pts',(13.2895844285102,0.43987294442654,3.85204173475342));
#35492=CARTESIAN_POINT('Ctrl Pts',(13.2974558005602,0.458413520067676,3.92763357054259));
#35493=CARTESIAN_POINT('Ctrl Pts',(13.3053271726101,0.457903200829578,4.00309657448501));
#35494=CARTESIAN_POINT('Ctrl Pts',(13.3131985446601,0.457392881591479,4.07855957842742));
#35495=CARTESIAN_POINT('Ctrl Pts',(13.3210699167101,0.437831667474148,4.15389375052308));
#35496=CARTESIAN_POINT('Ctrl Pts',(13.32894128876,0.401563549045306,4.22007191138728));
#35497=CARTESIAN_POINT('Ctrl Pts',(13.33681266081,0.365295430616463,4.28625007225149));
#35498=CARTESIAN_POINT('Ctrl Pts',(13.3446840328599,0.31232040787611,4.34327222188425));
#35499=CARTESIAN_POINT('Ctrl Pts',(13.3525554049099,0.248986397312635,4.38430548273058));
#35500=CARTESIAN_POINT('Ctrl Pts',(13.3604267769598,0.185652386749161,4.42533874357692));
#35501=CARTESIAN_POINT('Ctrl Pts',(13.3682981490098,0.111959388362564,4.45038311563682));
#35502=CARTESIAN_POINT('Ctrl Pts',(13.3761695210597,0.0367379221854645,
4.45643756985705));
#35503=CARTESIAN_POINT('Ctrl Pts',(13.3774477778781,0.024522472144774,4.45742077168506));
#35504=CARTESIAN_POINT('Ctrl Pts',(13.3787260346965,0.0122667140672706,
4.45790318029249));
#35505=CARTESIAN_POINT('Ctrl Pts',(13.3800042915148,1.00338821889499E-5,
4.45789143379912));
#35506=CARTESIAN_POINT('Origin',(12.5,0.,4.));
#35507=CARTESIAN_POINT('',(13.6800042915148,-8.85210990424201E-6,4.45789764648838));
#35508=CARTESIAN_POINT('',(13.5699957084852,1.03170790782398E-5,4.4578580083501));
#35509=CARTESIAN_POINT('',(12.5,-5.60735153159594E-17,4.457875));
#35510=CARTESIAN_POINT('Ctrl Pts',(13.5699957084852,1.03170790782398E-5,
4.4578580083501));
#35511=CARTESIAN_POINT('Ctrl Pts',(13.5675422145714,0.0235408097699949,
4.45787795556699));
#35512=CARTESIAN_POINT('Ctrl Pts',(13.5650887206577,0.0470683081483061,
4.45609516914004));
#35513=CARTESIAN_POINT('Ctrl Pts',(13.562635226744,0.0703115975725277,4.45248338388903));
#35514=CARTESIAN_POINT('Ctrl Pts',(13.554763854694,0.144881409096958,4.44089594716616));
#35515=CARTESIAN_POINT('Ctrl Pts',(13.5468924826441,0.21652593236894,4.41048310506186));
#35516=CARTESIAN_POINT('Ctrl Pts',(13.5390211105941,0.276660113016528,4.36488918223832));
#35517=CARTESIAN_POINT('Ctrl Pts',(13.5311497385442,0.336794293664116,4.31929525941478));
#35518=CARTESIAN_POINT('Ctrl Pts',(13.5232783664942,0.385418131687311,4.25852025587201));
#35519=CARTESIAN_POINT('Ctrl Pts',(13.5154069944443,0.416705106451492,4.18984674794718));
#35520=CARTESIAN_POINT('Ctrl Pts',(13.5075356223943,0.447992081215673,4.12117324002235));
#35521=CARTESIAN_POINT('Ctrl Pts',(13.4996642503443,0.461942192720839,4.04460122771548));
#35522=CARTESIAN_POINT('Ctrl Pts',(13.4917928782944,0.456883820300162,3.96930621892307));
#35523=CARTESIAN_POINT('Ctrl Pts',(13.4839215062444,0.451825447879485,3.89401121013066));
#35524=CARTESIAN_POINT('Ctrl Pts',(13.4760501341945,0.427758591532965,3.81999320485271));
#35525=CARTESIAN_POINT('Ctrl Pts',(13.4681787621445,0.387567146091087,3.75612166820384));
#35526=CARTESIAN_POINT('Ctrl Pts',(13.4603073900946,0.347375700649209,3.69225013155497));
#35527=CARTESIAN_POINT('Ctrl Pts',(13.4524360180446,0.291059666111973,3.63852506353517));
#35528=CARTESIAN_POINT('Ctrl Pts',(13.4445646459947,0.225367307335285,3.60138425741911));
#35529=CARTESIAN_POINT('Ctrl Pts',(13.4366932739447,0.159674948558598,3.56424345130305));
#35530=CARTESIAN_POINT('Ctrl Pts',(13.4288219018947,0.0846062655424597,
3.54368690709073));
#35531=CARTESIAN_POINT('Ctrl Pts',(13.4209505298448,0.00915662451852634,
3.54217788424291));
#35532=CARTESIAN_POINT('Ctrl Pts',(13.4130791577948,-0.0662930165054059,
3.54066886139509));
#35533=CARTESIAN_POINT('Ctrl Pts',(13.4052077857449,-0.142123615537132,
3.55820735991178));
#35534=CARTESIAN_POINT('Ctrl Pts',(13.3973364136949,-0.209248507106454,
3.5926917681625));
#35535=CARTESIAN_POINT('Ctrl Pts',(13.389465041645,-0.276373398675776,3.62717617641322));
#35536=CARTESIAN_POINT('Ctrl Pts',(13.381593669595,-0.334792582782693,3.67860649439798));
#35537=CARTESIAN_POINT('Ctrl Pts',(13.3737222975451,-0.377505777353741,
3.74081990525232));
#35538=CARTESIAN_POINT('Ctrl Pts',(13.3658509254951,-0.420218971924789,
3.80303331610666));
#35539=CARTESIAN_POINT('Ctrl Pts',(13.3579795534451,-0.44722617695997,3.87602981983059));
#35540=CARTESIAN_POINT('Ctrl Pts',(13.3501081813952,-0.455291160112798,
3.95106235628872));
#35541=CARTESIAN_POINT('Ctrl Pts',(13.3422368093452,-0.463356143265626,
4.02609489274685));
#35542=CARTESIAN_POINT('Ctrl Pts',(13.3343654372953,-0.452478904536101,
4.10316346193917));
#35543=CARTESIAN_POINT('Ctrl Pts',(13.3264940652453,-0.423962846915058,
4.17303305431203));
#35544=CARTESIAN_POINT('Ctrl Pts',(13.3186226931954,-0.395446789294015,
4.24290264668488));
#35545=CARTESIAN_POINT('Ctrl Pts',(13.3107513211454,-0.349291912781453,
4.30557326223827));
#35546=CARTESIAN_POINT('Ctrl Pts',(13.3028799490955,-0.291028886105345,
4.35353517632783));
#35547=CARTESIAN_POINT('Ctrl Pts',(13.2950085770455,-0.232765859429236,
4.4014970904174));
#35548=CARTESIAN_POINT('Ctrl Pts',(13.2871372049956,-0.162394682589579,
4.43475030304313));
#35549=CARTESIAN_POINT('Ctrl Pts',(13.2792658329456,-0.0883478267899694,
4.44931013225873));
#35550=CARTESIAN_POINT('Ctrl Pts',(13.2761757914588,-0.059279469337623,
4.4550258417985));
#35551=CARTESIAN_POINT('Ctrl Pts',(13.273085749972,-0.0296446570187532,
4.45786073445524));
#35552=CARTESIAN_POINT('Ctrl Pts',(13.2699957084852,-6.83105689078257E-6,
4.45784477598907));
#35553=CARTESIAN_POINT('Ctrl Pts',(13.3800042915148,1.00338821889499E-5,
4.45789143379912));
#35554=CARTESIAN_POINT('Ctrl Pts',(13.3865974067464,-0.0632086430349686,
4.45783084661254));
#35555=CARTESIAN_POINT('Ctrl Pts',(13.393190521978,-0.12645185159805,4.44462381290384));
#35556=CARTESIAN_POINT('Ctrl Pts',(13.3997836372096,-0.184315051738561,
4.41918121595096));
#35557=CARTESIAN_POINT('Ctrl Pts',(13.4076550092596,-0.253396625517876,
4.3888058714441));
#35558=CARTESIAN_POINT('Ctrl Pts',(13.4155263813095,-0.314809839108902,
4.34099064604983));
#35559=CARTESIAN_POINT('Ctrl Pts',(13.4233977533595,-0.361195640434018,
4.28146516557999));
#35560=CARTESIAN_POINT('Ctrl Pts',(13.4312691254094,-0.407581441759134,
4.22193968511016));
#35561=CARTESIAN_POINT('Ctrl Pts',(13.4391404974594,-0.438939830818339,
4.15070394956476));
#35562=CARTESIAN_POINT('Ctrl Pts',(13.4470118695093,-0.451513179494438,
4.07629402890356));
#35563=CARTESIAN_POINT('Ctrl Pts',(13.4548832415593,-0.464086528170537,
4.00188410824235));
#35564=CARTESIAN_POINT('Ctrl Pts',(13.4627546136093,-0.457874836463529,
3.92430000246534));
#35565=CARTESIAN_POINT('Ctrl Pts',(13.4706259856592,-0.433622441953051,
3.85283849709185));
#35566=CARTESIAN_POINT('Ctrl Pts',(13.4784973577092,-0.409370047442573,
3.78137699171835));
#35567=CARTESIAN_POINT('Ctrl Pts',(13.4863687297591,-0.367076950128625,
3.71603808674838));
#35568=CARTESIAN_POINT('Ctrl Pts',(13.4942401018091,-0.311811067605128,
3.66465124389307));
#35569=CARTESIAN_POINT('Ctrl Pts',(13.502111473859,-0.25654518508163,3.61326440103776));
#35570=CARTESIAN_POINT('Ctrl Pts',(13.509982845909,-0.188306517348584,3.5758296202971));
#35571=CARTESIAN_POINT('Ctrl Pts',(13.5178542179589,-0.115272000283325,
3.55683265457144));
#35572=CARTESIAN_POINT('Ctrl Pts',(13.5257255900089,-0.0422374832180674,
3.53783568884578));
#35573=CARTESIAN_POINT('Ctrl Pts',(13.5335969620589,0.035592883179403,3.53727653813511));
#35574=CARTESIAN_POINT('Ctrl Pts',(13.5414683341088,0.108892804353757,3.55522220461956));
#35575=CARTESIAN_POINT('Ctrl Pts',(13.5493397061588,0.182192725528112,3.573167871104));
#35576=CARTESIAN_POINT('Ctrl Pts',(13.5572110782087,0.250962201479351,3.60961835478357));
#35577=CARTESIAN_POINT('Ctrl Pts',(13.5650824502587,0.306960690387823,3.66020584957927));
#35578=CARTESIAN_POINT('Ctrl Pts',(13.5729538223086,0.362959179296295,3.71079334437498));
#35579=CARTESIAN_POINT('Ctrl Pts',(13.5808251943586,0.406186681162,3.77551785028682));
#35580=CARTESIAN_POINT('Ctrl Pts',(13.5886965664085,0.431463310113251,3.84662352810933));
#35581=CARTESIAN_POINT('Ctrl Pts',(13.5965679384585,0.456739939064502,3.91772920593184));
#35582=CARTESIAN_POINT('Ctrl Pts',(13.6044393105085,0.464065695101298,3.99521605566501));
#35583=CARTESIAN_POINT('Ctrl Pts',(13.6123106825584,0.452562744007997,4.06979894583348));
#35584=CARTESIAN_POINT('Ctrl Pts',(13.6201820546084,0.441059792914696,4.14438183600196));
#35585=CARTESIAN_POINT('Ctrl Pts',(13.6280534266583,0.410728134691299,4.21606076660573));
#35586=CARTESIAN_POINT('Ctrl Pts',(13.6359247987083,0.365202365858889,4.27624656029457));
#35587=CARTESIAN_POINT('Ctrl Pts',(13.6437961707582,0.319676597026479,4.33643235398341));
#35588=CARTESIAN_POINT('Ctrl Pts',(13.6516675428082,0.258956717585058,4.38512501075732));
#35589=CARTESIAN_POINT('Ctrl Pts',(13.6595389148581,0.190318698434502,4.41648976353532));
#35590=CARTESIAN_POINT('Ctrl Pts',(13.666360707077,0.130832969391341,4.44367229602021));
#35591=CARTESIAN_POINT('Ctrl Pts',(13.6731824992959,0.065399948454096,4.45783988979956));
#35592=CARTESIAN_POINT('Ctrl Pts',(13.6800042915148,-8.85210990424201E-6,
4.45789764648838));
#35593=CARTESIAN_POINT('Origin',(12.5,0.,4.));
#35594=CARTESIAN_POINT('',(13.9800042915148,-4.68615130337092E-6,4.45784092071359));
#35595=CARTESIAN_POINT('',(13.8699957084852,1.23414887176878E-6,4.4579133809027));
#35596=CARTESIAN_POINT('',(12.5,-5.60735153159594E-17,4.457875));
#35597=CARTESIAN_POINT('Ctrl Pts',(13.8699957084852,1.23414887176878E-6,
4.4579133809027));
#35598=CARTESIAN_POINT('Ctrl Pts',(13.8698700512209,0.00120594270822336,
4.45791357044259));
#35599=CARTESIAN_POINT('Ctrl Pts',(13.8697443939566,0.00241064979645091,
4.45790891401425));
#35600=CARTESIAN_POINT('Ctrl Pts',(13.8696187366923,0.00361531855258033,
4.45789940262096));
#35601=CARTESIAN_POINT('Ctrl Pts',(13.8617473646423,0.0790776965455978,
4.45730359373015));
#35602=CARTESIAN_POINT('Ctrl Pts',(13.8538759925924,0.154389660535011,4.43765704798318));
#35603=CARTESIAN_POINT('Ctrl Pts',(13.8460046205424,0.22052669229976,4.40131398110731));
#35604=CARTESIAN_POINT('Ctrl Pts',(13.8381332484924,0.286663724064511,4.36497091423144));
#35605=CARTESIAN_POINT('Ctrl Pts',(13.8302618764425,0.343625823604597,4.31193132622667));
#35606=CARTESIAN_POINT('Ctrl Pts',(13.8223905043925,0.384587309076409,4.24855087033892));
#35607=CARTESIAN_POINT('Ctrl Pts',(13.8145191323426,0.42554879454822,4.18517041445118));
#35608=CARTESIAN_POINT('Ctrl Pts',(13.8066477602926,0.450509665951756,4.11144909068046));
#35609=CARTESIAN_POINT('Ctrl Pts',(13.7987763882427,0.456478899990553,4.03622081324714));
#35610=CARTESIAN_POINT('Ctrl Pts',(13.7909050161927,0.46244813402935,3.96099253581381));
#35611=CARTESIAN_POINT('Ctrl Pts',(13.7830336441427,0.449425730703409,3.88425730471787));
#35612=CARTESIAN_POINT('Ctrl Pts',(13.7751622720928,0.418972144817937,3.81521018611534));
#35613=CARTESIAN_POINT('Ctrl Pts',(13.7672909000428,0.388518558932466,3.74616306751281));
#35614=CARTESIAN_POINT('Ctrl Pts',(13.7594195279929,0.340633790487464,3.68480406140369));
#35615=CARTESIAN_POINT('Ctrl Pts',(13.7515481559429,0.281055798532888,3.6384857242654));
#35616=CARTESIAN_POINT('Ctrl Pts',(13.743676783893,0.221477806578313,3.59216738712712));
#35617=CARTESIAN_POINT('Ctrl Pts',(13.735805411843,0.150206591114165,3.56088971895966));
#35618=CARTESIAN_POINT('Ctrl Pts',(13.7279340397931,0.0757824736049535,
3.54840067521841));
#35619=CARTESIAN_POINT('Ctrl Pts',(13.7200626677431,0.00135835609574232,
3.53591163147717));
#35620=CARTESIAN_POINT('Ctrl Pts',(13.7121912956931,-0.0762186634585312,
3.54221121216214));
#35621=CARTESIAN_POINT('Ctrl Pts',(13.7043199236432,-0.14765264866984,3.56654454809098));
#35622=CARTESIAN_POINT('Ctrl Pts',(13.6964485515932,-0.219086633881149,
3.59087788401983));
#35623=CARTESIAN_POINT('Ctrl Pts',(13.6885771795433,-0.284377584749494,
3.63324497519255));
#35624=CARTESIAN_POINT('Ctrl Pts',(13.6807058074933,-0.335701785830877,
3.68856903744356));
#35625=CARTESIAN_POINT('Ctrl Pts',(13.6728344354434,-0.38702598691226,3.74389309969457));
#35626=CARTESIAN_POINT('Ctrl Pts',(13.6649630633934,-0.424383438206683,
3.81217413302386));
#35627=CARTESIAN_POINT('Ctrl Pts',(13.6570916913435,-0.443297653083863,
3.88523012494906));
#35628=CARTESIAN_POINT('Ctrl Pts',(13.6492203192935,-0.462211867961044,
3.95828611687427));
#35629=CARTESIAN_POINT('Ctrl Pts',(13.6413489472436,-0.462682846420982,
4.03611706739538));
#35630=CARTESIAN_POINT('Ctrl Pts',(13.6334775751936,-0.444654151830396,
4.10939661196244));
#35631=CARTESIAN_POINT('Ctrl Pts',(13.6256062031436,-0.42662545723981,4.18267615652949));
#35632=CARTESIAN_POINT('Ctrl Pts',(13.6177348310937,-0.3900970895987,4.25140429514248));
#35633=CARTESIAN_POINT('Ctrl Pts',(13.6098634590437,-0.339446187702822,
4.3073454393722));
#35634=CARTESIAN_POINT('Ctrl Pts',(13.6019920869938,-0.288795285806945,
4.36328658360191));
#35635=CARTESIAN_POINT('Ctrl Pts',(13.5941207149438,-0.224021849656302,
4.40644073344835));
#35636=CARTESIAN_POINT('Ctrl Pts',(13.5862493428939,-0.152887581692542,
4.43163679270085));
#35637=CARTESIAN_POINT('Ctrl Pts',(13.5808314647576,-0.103925749791867,
4.44897928111035));
#35638=CARTESIAN_POINT('Ctrl Pts',(13.5754135866214,-0.0519504158054226,
4.45781396031326));
#35639=CARTESIAN_POINT('Ctrl Pts',(13.5699957084852,1.03170790782398E-5,
4.4578580083501));
#35640=CARTESIAN_POINT('Ctrl Pts',(13.6800042915148,-8.85210990424201E-6,
4.45789764648838));
#35641=CARTESIAN_POINT('Ctrl Pts',(13.6810538713459,-0.010072447664127,
4.45790653275371));
#35642=CARTESIAN_POINT('Ctrl Pts',(13.6821034511769,-0.0201354698749596,
4.45758141170421));
#35643=CARTESIAN_POINT('Ctrl Pts',(13.683153031008,-0.0301761699425476,
4.45691829561871));
#35644=CARTESIAN_POINT('Ctrl Pts',(13.691024403058,-0.105476860309351,4.45194522614199));
#35645=CARTESIAN_POINT('Ctrl Pts',(13.6988957751079,-0.179522082183268,
4.42796223840642));
#35646=CARTESIAN_POINT('Ctrl Pts',(13.7067671471579,-0.24343910912634,4.38784317739428));
#35647=CARTESIAN_POINT('Ctrl Pts',(13.7146385192078,-0.307356136069411,
4.34772411638213));
#35648=CARTESIAN_POINT('Ctrl Pts',(13.7225098912578,-0.361144968081636,
4.2914689820934));
#35649=CARTESIAN_POINT('Ctrl Pts',(13.7303812633077,-0.398360171146024,
4.22581874179975));
#35650=CARTESIAN_POINT('Ctrl Pts',(13.7382526353577,-0.435575374210412,
4.1601685015061));
#35651=CARTESIAN_POINT('Ctrl Pts',(13.7461240074077,-0.456216948326962,
4.08512315520753));
#35652=CARTESIAN_POINT('Ctrl Pts',(13.7539953794576,-0.457811445030669,
4.00967527273228));
#35653=CARTESIAN_POINT('Ctrl Pts',(13.7618667515076,-0.459405941734377,
3.93422739025703));
#35654=CARTESIAN_POINT('Ctrl Pts',(13.7697381235575,-0.441953361025241,
3.85837697160509));
#35655=CARTESIAN_POINT('Ctrl Pts',(13.7776094956075,-0.407545019133394,
3.79121305720166));
#35656=CARTESIAN_POINT('Ctrl Pts',(13.7854808676574,-0.373136677241547,
3.72404914279823));
#35657=CARTESIAN_POINT('Ctrl Pts',(13.7933522397074,-0.321772574166988,
3.6655717326433));
#35658=CARTESIAN_POINT('Ctrl Pts',(13.8012236117573,-0.259607592342073,
3.6227880859492));
#35659=CARTESIAN_POINT('Ctrl Pts',(13.8090949838073,-0.19744261051716,3.5800044392551));
#35660=CARTESIAN_POINT('Ctrl Pts',(13.8169663558573,-0.124476749941891,
3.55291455602183));
#35661=CARTESIAN_POINT('Ctrl Pts',(13.8248377279072,-0.0494533988297167,
3.54476457579874));
#35662=CARTESIAN_POINT('Ctrl Pts',(13.8327090999572,0.0255699522824598,
3.53661459557564));
#35663=CARTESIAN_POINT('Ctrl Pts',(13.8405804720071,0.102650793931542,3.54740451836272));
#35664=CARTESIAN_POINT('Ctrl Pts',(13.8484518440571,0.172552645974024,3.57584140410587));
#35665=CARTESIAN_POINT('Ctrl Pts',(13.856323216107,0.242454498016503,3.60427828984902));
#35666=CARTESIAN_POINT('Ctrl Pts',(13.864194588157,0.305177360452382,3.65036213854823));
#35667=CARTESIAN_POINT('Ctrl Pts',(13.8720659602069,0.353205247972751,3.70857079263049));
#35668=CARTESIAN_POINT('Ctrl Pts',(13.8799373322569,0.40123313549312,3.76677944671275));
#35669=CARTESIAN_POINT('Ctrl Pts',(13.8878087043068,0.434566048097978,3.83711290617806));
#35670=CARTESIAN_POINT('Ctrl Pts',(13.8956800763568,0.44920975351361,3.9111432194385));
#35671=CARTESIAN_POINT('Ctrl Pts',(13.9035514484068,0.463853458929242,3.98517353269893));
#35672=CARTESIAN_POINT('Ctrl Pts',(13.9114228204567,0.459807957155645,4.06290069975448));
#35673=CARTESIAN_POINT('Ctrl Pts',(13.9192941925067,0.437558014523894,4.13501079227018));
#35674=CARTESIAN_POINT('Ctrl Pts',(13.9271655645566,0.415308071892144,4.20712088478587));
#35675=CARTESIAN_POINT('Ctrl Pts',(13.9350369366066,0.374853688402242,4.27361390276169));
#35676=CARTESIAN_POINT('Ctrl Pts',(13.9429083086565,0.321042451364188,4.32652208887851));
#35677=CARTESIAN_POINT('Ctrl Pts',(13.9507796807065,0.267231214326134,4.37943027499533));
#35678=CARTESIAN_POINT('Ctrl Pts',(13.9586510527564,0.200063123739928,4.41875362925314));
#35679=CARTESIAN_POINT('Ctrl Pts',(13.9665224248064,0.127586829849962,4.43978009385641));
#35680=CARTESIAN_POINT('Ctrl Pts',(13.9710163803759,0.086208370984788,4.45178460807712));
#35681=CARTESIAN_POINT('Ctrl Pts',(13.9755103359454,0.0430996806131821,
4.45782517307841));
#35682=CARTESIAN_POINT('Ctrl Pts',(13.9800042915148,-4.68615130337092E-6,
4.45784092071359));
#35683=CARTESIAN_POINT('Origin',(12.5,0.,4.));
#35684=CARTESIAN_POINT('',(14.2800042915148,1.11332528513013E-5,4.45786561359635));
#35685=CARTESIAN_POINT('',(14.1699957084852,-1.10604184835328E-5,4.4578646218584));
#35686=CARTESIAN_POINT('',(12.5,-5.60735153159594E-17,4.457875));
#35687=CARTESIAN_POINT('Ctrl Pts',(14.1699957084852,-1.10604184835328E-5,
4.4578646218584));
#35688=CARTESIAN_POINT('Ctrl Pts',(14.1643265158203,0.0543576752587709,
4.45781404039958));
#35689=CARTESIAN_POINT('Ctrl Pts',(14.1586573231555,0.108743966382031,4.44812254260427));
#35690=CARTESIAN_POINT('Ctrl Pts',(14.1529881304907,0.159684023833442,4.42916890146099));
#35691=CARTESIAN_POINT('Ctrl Pts',(14.1451167584407,0.230411580321883,4.40285278028461));
#35692=CARTESIAN_POINT('Ctrl Pts',(14.1372453863907,0.294495541512382,4.358681244225));
#35693=CARTESIAN_POINT('Ctrl Pts',(14.1293740143408,0.344256823700223,4.30194730133701));
#35694=CARTESIAN_POINT('Ctrl Pts',(14.1215026422908,0.394018105888063,4.24521335844902));
#35695=CARTESIAN_POINT('Ctrl Pts',(14.1136312702409,0.429456709073245,4.17591700873265));
#35696=CARTESIAN_POINT('Ctrl Pts',(14.1057598981909,0.446326079279053,4.10236192849032));
#35697=CARTESIAN_POINT('Ctrl Pts',(14.097888526141,0.46319544948486,4.02880684824799));
#35698=CARTESIAN_POINT('Ctrl Pts',(14.090017154091,0.461495586711293,3.95099303747972));
#35699=CARTESIAN_POINT('Ctrl Pts',(14.0821457820411,0.441430182931853,3.87824480690492));
#35700=CARTESIAN_POINT('Ctrl Pts',(14.0742744099911,0.421364779152413,3.80549657633012));
#35701=CARTESIAN_POINT('Ctrl Pts',(14.0664030379411,0.3829338343671,3.73781392594881));
#35702=CARTESIAN_POINT('Ctrl Pts',(14.0585316658912,0.330742470300218,3.68330716492384));
#35703=CARTESIAN_POINT('Ctrl Pts',(14.0506602938412,0.278551106233337,3.62880040389886));
#35704=CARTESIAN_POINT('Ctrl Pts',(14.0427889217913,0.212599322884887,3.58746953223022));
#35705=CARTESIAN_POINT('Ctrl Pts',(14.0349175497413,0.140790022250932,3.5642671654747));
#35706=CARTESIAN_POINT('Ctrl Pts',(14.0270461776914,0.0689807216169763,
3.54106479871918));
#35707=CARTESIAN_POINT('Ctrl Pts',(14.0191748056414,-0.00868609630248519,
3.53599093687678));
#35708=CARTESIAN_POINT('Ctrl Pts',(14.0113034335915,-0.0829037347177578,
3.5496535731032));
#35709=CARTESIAN_POINT('Ctrl Pts',(14.0034320615415,-0.15712137313303,3.56331620932962));
#35710=CARTESIAN_POINT('Ctrl Pts',(13.9955606894916,-0.227889832044114,
3.59571534362485));
#35711=CARTESIAN_POINT('Ctrl Pts',(13.9876893174416,-0.286729034540398,
3.64296863695132));
#35712=CARTESIAN_POINT('Ctrl Pts',(13.9798179453916,-0.345568237036683,
3.69022193027778));
#35713=CARTESIAN_POINT('Ctrl Pts',(13.9719465733417,-0.392478183118168,
3.75232938263547));
#35714=CARTESIAN_POINT('Ctrl Pts',(13.9640752012917,-0.421837725217638,
3.82184875237013));
#35715=CARTESIAN_POINT('Ctrl Pts',(13.9562038292418,-0.451197267317109,
3.8913681221048));
#35716=CARTESIAN_POINT('Ctrl Pts',(13.9483324571918,-0.463006405434566,
3.96829940921644));
#35717=CARTESIAN_POINT('Ctrl Pts',(13.9404610851419,-0.455850068491383,
4.04342405445454));
#35718=CARTESIAN_POINT('Ctrl Pts',(13.9325897130919,-0.448693731548199,
4.11854869969265));
#35719=CARTESIAN_POINT('Ctrl Pts',(13.924718341042,-0.422571919544373,4.19186670305722));
#35720=CARTESIAN_POINT('Ctrl Pts',(13.916846968992,-0.38061476952465,4.25459247959939));
#35721=CARTESIAN_POINT('Ctrl Pts',(13.908975596942,-0.338657619504927,4.31731825614156));
#35722=CARTESIAN_POINT('Ctrl Pts',(13.9011042248921,-0.280865131469307,
4.36945180586132));
#35723=CARTESIAN_POINT('Ctrl Pts',(13.8932328528421,-0.214162491453186,
4.40474604470388));
#35724=CARTESIAN_POINT('Ctrl Pts',(13.8854871380565,-0.148524681204106,
4.43947685223224));
#35725=CARTESIAN_POINT('Ctrl Pts',(13.8777414232708,-0.0742589286223064,
4.45790169736071));
#35726=CARTESIAN_POINT('Ctrl Pts',(13.8699957084852,1.23414887176878E-6,
4.4579133809027));
#35727=CARTESIAN_POINT('Ctrl Pts',(13.9800042915148,-4.68615130337092E-6,
4.45784092071359));
#35728=CARTESIAN_POINT('Ctrl Pts',(13.9833817079953,-0.0323996211791616,
4.45785275579335));
#35729=CARTESIAN_POINT('Ctrl Pts',(13.9867591244758,-0.064792114138131,
4.45446164082457));
#35730=CARTESIAN_POINT('Ctrl Pts',(13.9901365409563,-0.0964458636128916,
4.44764173788363));
#35731=CARTESIAN_POINT('Ctrl Pts',(13.9980079130062,-0.170217765992045,
4.43174734235885));
#35732=CARTESIAN_POINT('Ctrl Pts',(14.0058792850562,-0.239977073556624,
4.39722897636055));
#35733=CARTESIAN_POINT('Ctrl Pts',(14.0137506571061,-0.297364634468633,
4.34822292324149));
#35734=CARTESIAN_POINT('Ctrl Pts',(14.0216220291561,-0.354752195380644,
4.29921687012243));
#35735=CARTESIAN_POINT('Ctrl Pts',(14.0294934012061,-0.399768009640084,
4.23572312988262));
#35736=CARTESIAN_POINT('Ctrl Pts',(14.037364773256,-0.427017900618165,4.16535006094698));
#35737=CARTESIAN_POINT('Ctrl Pts',(14.045236145306,-0.454267791596245,4.09497699201134));
#35738=CARTESIAN_POINT('Ctrl Pts',(14.0531075173559,-0.463751759292965,
4.01772459437987));
#35739=CARTESIAN_POINT('Ctrl Pts',(14.0609788894059,-0.45433335426851,3.94284990548881));
#35740=CARTESIAN_POINT('Ctrl Pts',(14.0688502614558,-0.444914949244056,
3.86797521659775));
#35741=CARTESIAN_POINT('Ctrl Pts',(14.0767216335058,-0.416594171498428,
3.7954782364471));
#35742=CARTESIAN_POINT('Ctrl Pts',(14.0845930055557,-0.372764656800254,
3.7340461680214));
#35743=CARTESIAN_POINT('Ctrl Pts',(14.0924643776057,-0.328935142102078,
3.67261409959569));
#35744=CARTESIAN_POINT('Ctrl Pts',(14.1003357496557,-0.269596890451354,
3.62224694289495));
#35745=CARTESIAN_POINT('Ctrl Pts',(14.1082071217056,-0.201860314388951,
3.58898011778223));
#35746=CARTESIAN_POINT('Ctrl Pts',(14.1160784937556,-0.134123738326549,
3.55571329266952));
#35747=CARTESIAN_POINT('Ctrl Pts',(14.1239498658055,-0.0579888378524715,
3.53954679914483));
#35748=CARTESIAN_POINT('Ctrl Pts',(14.1318212378555,0.0174212575835846,
3.54241784356498));
#35749=CARTESIAN_POINT('Ctrl Pts',(14.1396926099054,0.0928313530196406,
3.54528888798513));
#35750=CARTESIAN_POINT('Ctrl Pts',(14.1475639819554,0.167516643417675,3.56719747035013));
#35751=CARTESIAN_POINT('Ctrl Pts',(14.1554353540053,0.232527703900953,3.60551831852155));
#35752=CARTESIAN_POINT('Ctrl Pts',(14.1633067260553,0.297538764384231,3.64383916669297));
#35753=CARTESIAN_POINT('Ctrl Pts',(14.1711780981053,0.352875594952755,3.69857228067082));
#35754=CARTESIAN_POINT('Ctrl Pts',(14.1790494701552,0.391907267274456,3.76315907456484));
#35755=CARTESIAN_POINT('Ctrl Pts',(14.1869208422052,0.430938939596158,3.82774586845886));
#35756=CARTESIAN_POINT('Ctrl Pts',(14.1947922142551,0.453665453671035,3.90218634226906));
#35757=CARTESIAN_POINT('Ctrl Pts',(14.2026635863051,0.45736352584659,3.97756040711846));
#35758=CARTESIAN_POINT('Ctrl Pts',(14.210534958355,0.461061598022145,4.05293447196787));
#35759=CARTESIAN_POINT('Ctrl Pts',(14.218406330405,0.445731228298378,4.12924212785648));
#35760=CARTESIAN_POINT('Ctrl Pts',(14.2262777024549,0.413209431587385,4.19733954431574));
#35761=CARTESIAN_POINT('Ctrl Pts',(14.2341490745049,0.380687634876391,4.265436960775));
#35762=CARTESIAN_POINT('Ctrl Pts',(14.2420204465549,0.330974411178171,4.32532413780492));
#35763=CARTESIAN_POINT('Ctrl Pts',(14.2498918186048,0.270026820557645,4.36982488597043));
#35764=CARTESIAN_POINT('Ctrl Pts',(14.2577631906548,0.209079229937118,4.41432563413594));
#35765=CARTESIAN_POINT('Ctrl Pts',(14.2656345627047,0.136897272394287,4.44343995343705));
#35766=CARTESIAN_POINT('Ctrl Pts',(14.2735059347547,0.0621304022332317,
4.45367911922619));
#35767=CARTESIAN_POINT('Ctrl Pts',(14.2756720536747,0.0415553447945806,
4.4564968301158));
#35768=CARTESIAN_POINT('Ctrl Pts',(14.2778381725948,0.020784533837212,4.45788513960506));
#35769=CARTESIAN_POINT('Ctrl Pts',(14.2800042915148,1.11332528513013E-5,
4.45786561359635));
#35770=CARTESIAN_POINT('Origin',(12.5,0.,4.));
#35771=CARTESIAN_POINT('',(14.5800042915148,-1.58578451148518E-6,4.45791318879952));
#35772=CARTESIAN_POINT('',(14.4699957084852,4.96934848862042E-6,4.4578413260902));
#35773=CARTESIAN_POINT('',(12.5,-5.60735153159594E-17,4.457875));
#35774=CARTESIAN_POINT('Ctrl Pts',(14.4699957084852,4.96934848862042E-6,
4.4578413260902));
#35775=CARTESIAN_POINT('Ctrl Pts',(14.4666543524698,0.0320539454002899,
4.45785375637851));
#35776=CARTESIAN_POINT('Ctrl Pts',(14.4633129964543,0.0641003838712636,
4.45453523052653));
#35777=CARTESIAN_POINT('Ctrl Pts',(14.4599716404389,0.0954313752779353,
4.44785911407655));
#35778=CARTESIAN_POINT('Ctrl Pts',(14.452100268389,0.169239101517837,4.43213190746217));
#35779=CARTESIAN_POINT('Ctrl Pts',(14.444228896339,0.2390764403586,4.39777168651743));
#35780=CARTESIAN_POINT('Ctrl Pts',(14.4363575242891,0.296574889592956,4.34889578431359));
#35781=CARTESIAN_POINT('Ctrl Pts',(14.4284861522391,0.354073338827311,4.30001988210975));
#35782=CARTESIAN_POINT('Ctrl Pts',(14.4206147801891,0.39923289845526,4.2366282986468));
#35783=CARTESIAN_POINT('Ctrl Pts',(14.4127434081392,0.4266421670589,4.16631715105832));
#35784=CARTESIAN_POINT('Ctrl Pts',(14.4048720360892,0.454051435662541,4.09600600346984));
#35785=CARTESIAN_POINT('Ctrl Pts',(14.3970006640393,0.463710413241873,4.01877529175582));
#35786=CARTESIAN_POINT('Ctrl Pts',(14.3891292919893,0.454461679188747,3.94387945476197));
#35787=CARTESIAN_POINT('Ctrl Pts',(14.3812579199394,0.445212945135621,3.86898361776811));
#35788=CARTESIAN_POINT('Ctrl Pts',(14.3733865478894,0.417056499450037,3.79642265549441));
#35789=CARTESIAN_POINT('Ctrl Pts',(14.3655151758395,0.373366286239542,3.73489143780602));
#35790=CARTESIAN_POINT('Ctrl Pts',(14.3576438037895,0.329676073029047,3.67336022011762));
#35791=CARTESIAN_POINT('Ctrl Pts',(14.3497724317395,0.270452092293641,3.62285874701452));
#35792=CARTESIAN_POINT('Ctrl Pts',(14.3419010596896,0.202791063664024,3.58943853329022));
#35793=CARTESIAN_POINT('Ctrl Pts',(14.3340296876396,0.135130035034407,3.55601831956592));
#35794=CARTESIAN_POINT('Ctrl Pts',(14.3261583155897,0.0590319585105798,
3.53967936522043));
#35795=CARTESIAN_POINT('Ctrl Pts',(14.3182869435397,-0.0163844490157649,
3.54237954232867));
#35796=CARTESIAN_POINT('Ctrl Pts',(14.3104155714898,-0.0918008565421096,
3.54507971943691));
#35797=CARTESIAN_POINT('Ctrl Pts',(14.3025441994398,-0.166535595070972,
3.56681902799889));
#35798=CARTESIAN_POINT('Ctrl Pts',(14.2946728273899,-0.231633314431234,
3.60499247969884));
#35799=CARTESIAN_POINT('Ctrl Pts',(14.2868014553399,-0.296731033791496,
3.64316593139879));
#35800=CARTESIAN_POINT('Ctrl Pts',(14.2789300832899,-0.352191733983158,
3.6977735262367));
#35801=CARTESIAN_POINT('Ctrl Pts',(14.27105871124,-0.391369643565407,3.76227171909014));
#35802=CARTESIAN_POINT('Ctrl Pts',(14.26318733919,-0.430547553147657,3.82676991194359));
#35803=CARTESIAN_POINT('Ctrl Pts',(14.2553159671401,-0.453442672120494,
3.90115870281258));
#35804=CARTESIAN_POINT('Ctrl Pts',(14.2474445950901,-0.457311513162664,
3.97652419590847));
#35805=CARTESIAN_POINT('Ctrl Pts',(14.2395732230402,-0.461180354204834,
4.05188968900435));
#35806=CARTESIAN_POINT('Ctrl Pts',(14.2317018509902,-0.446022917316338,
4.12823188432714));
#35807=CARTESIAN_POINT('Ctrl Pts',(14.2238304789403,-0.413655495130362,
4.19640281260034));
#35808=CARTESIAN_POINT('Ctrl Pts',(14.2159591068903,-0.381288072944386,
4.26457374087354));
#35809=CARTESIAN_POINT('Ctrl Pts',(14.2080877348403,-0.33171066546093,4.32457340209717));
#35810=CARTESIAN_POINT('Ctrl Pts',(14.2002163627904,-0.270864058094251,
4.36921212802613));
#35811=CARTESIAN_POINT('Ctrl Pts',(14.1923449907404,-0.210017450727571,
4.41385085395509));
#35812=CARTESIAN_POINT('Ctrl Pts',(14.1844736186905,-0.137901643477669,
4.44312864458938));
#35813=CARTESIAN_POINT('Ctrl Pts',(14.1766022466405,-0.0631581639595259,
4.45353718675995));
#35814=CARTESIAN_POINT('Ctrl Pts',(14.1744000672554,-0.0422471272657682,
4.45644919204336));
#35815=CARTESIAN_POINT('Ctrl Pts',(14.1721978878703,-0.021130418320356,
4.45788427006097));
#35816=CARTESIAN_POINT('Ctrl Pts',(14.1699957084852,-1.10604184835328E-5,
4.4578646218584));
#35817=CARTESIAN_POINT('Ctrl Pts',(14.2800042915148,1.11332528513013E-5,
4.45786561359635));
#35818=CARTESIAN_POINT('Ctrl Pts',(14.2857095446447,-0.0547030874695854,
4.45781418483069));
#35819=CARTESIAN_POINT('Ctrl Pts',(14.2914147977746,-0.109435272994953,
4.44799629651036));
#35820=CARTESIAN_POINT('Ctrl Pts',(14.2971200509045,-0.16065599949712,4.42880599334559));
#35821=CARTESIAN_POINT('Ctrl Pts',(14.3049914229545,-0.231323748287136,
4.40232968939868));
#35822=CARTESIAN_POINT('Ctrl Pts',(14.3128627950045,-0.295307463087888,
4.35801306922771));
#35823=CARTESIAN_POINT('Ctrl Pts',(14.3207341670544,-0.344940072567234,
4.30116652609615));
#35824=CARTESIAN_POINT('Ctrl Pts',(14.3286055391044,-0.394572682046581,
4.24431998296459));
#35825=CARTESIAN_POINT('Ctrl Pts',(14.3364769111543,-0.429854186204522,
4.17494351687244));
#35826=CARTESIAN_POINT('Ctrl Pts',(14.3443482832043,-0.446556856002091,
4.10135040434572));
#35827=CARTESIAN_POINT('Ctrl Pts',(14.3522196552542,-0.46325952579966,4.027757291819));
#35828=CARTESIAN_POINT('Ctrl Pts',(14.3600910273042,-0.461383361236856,
3.9499475328577));
#35829=CARTESIAN_POINT('Ctrl Pts',(14.3679623993541,-0.441153180262727,
3.87724495265939));
#35830=CARTESIAN_POINT('Ctrl Pts',(14.3758337714041,-0.420922999288597,
3.80454237246108));
#35831=CARTESIAN_POINT('Ctrl Pts',(14.383705143454,-0.382338801903142,3.73694697102576));
#35832=CARTESIAN_POINT('Ctrl Pts',(14.391576515504,-0.330024073856894,3.68255860260764));
#35833=CARTESIAN_POINT('Ctrl Pts',(14.399447887554,-0.277709345810648,3.62817023418952));
#35834=CARTESIAN_POINT('Ctrl Pts',(14.4073192596039,-0.21166408710361,3.58698889878861));
#35835=CARTESIAN_POINT('Ctrl Pts',(14.4151906316539,-0.139802400742051,
3.56394929325792));
#35836=CARTESIAN_POINT('Ctrl Pts',(14.4230620037038,-0.0679407143804897,
3.54090968772722));
#35837=CARTESIAN_POINT('Ctrl Pts',(14.4309333757538,0.00973739963559066,
3.53601181206673));
#35838=CARTESIAN_POINT('Ctrl Pts',(14.4388047478037,0.0839238909224197,
3.54984257127538));
#35839=CARTESIAN_POINT('Ctrl Pts',(14.4466761198537,0.158110382209248,3.56367333048403));
#35840=CARTESIAN_POINT('Ctrl Pts',(14.4545474919037,0.228805250766822,3.59623272456181));
#35841=CARTESIAN_POINT('Ctrl Pts',(14.4624188639536,0.287537237904754,3.64361921078484));
#35842=CARTESIAN_POINT('Ctrl Pts',(14.4702902360036,0.346269225042686,3.69100569700788));
#35843=CARTESIAN_POINT('Ctrl Pts',(14.4781616080535,0.393038330760977,3.75321927537615));
#35844=CARTESIAN_POINT('Ctrl Pts',(14.4860329801035,0.422240284179214,3.8228049873169));
#35845=CARTESIAN_POINT('Ctrl Pts',(14.4939043521534,0.451442237597453,3.89239069925764));
#35846=CARTESIAN_POINT('Ctrl Pts',(14.5017757242034,0.463077038715637,3.96934854477086));
#35847=CARTESIAN_POINT('Ctrl Pts',(14.5096470962533,0.45575050699275,4.04445678215295));
#35848=CARTESIAN_POINT('Ctrl Pts',(14.5175184683033,0.448423975269863,4.11956501953505));
#35849=CARTESIAN_POINT('Ctrl Pts',(14.5253898403532,0.422136110705906,4.19282364878603));
#35850=CARTESIAN_POINT('Ctrl Pts',(14.5332612124032,0.380036948171907,4.2554541996672));
#35851=CARTESIAN_POINT('Ctrl Pts',(14.5411325844532,0.337937785637909,4.31808475054837));
#35852=CARTESIAN_POINT('Ctrl Pts',(14.5490039565031,0.28002732513387,4.37008722305972));
#35853=CARTESIAN_POINT('Ctrl Pts',(14.5568753285531,0.213244889156206,4.40523023992844));
#35854=CARTESIAN_POINT('Ctrl Pts',(14.5645849828737,0.147834501639678,4.43965124177167));
#35855=CARTESIAN_POINT('Ctrl Pts',(14.5722946371942,0.0739129441497101,
4.45789842831743));
#35856=CARTESIAN_POINT('Ctrl Pts',(14.5800042915148,-1.58578451148518E-6,
4.45791318879952));
#35857=CARTESIAN_POINT('Origin',(12.5,0.,4.));
#35858=CARTESIAN_POINT('',(14.8800042915148,-1.01702808208336E-5,4.45785711824254));
#35859=CARTESIAN_POINT('',(14.7699957084852,8.6346448269735E-6,4.45789857801605));
#35860=CARTESIAN_POINT('',(12.5,-5.60735153159594E-17,4.457875));
#35861=CARTESIAN_POINT('Ctrl Pts',(14.7699957084852,8.6346448269735E-6,
4.45789857801605));
#35862=CARTESIAN_POINT('Ctrl Pts',(14.7689821891192,0.00972641784825355,
4.45790700998655));
#35863=CARTESIAN_POINT('Ctrl Pts',(14.7679686697532,0.01944367562558,4.45760386164098));
#35864=CARTESIAN_POINT('Ctrl Pts',(14.7669551503872,0.0291408329004781,
4.45698549795522));
#35865=CARTESIAN_POINT('Ctrl Pts',(14.7590837783372,0.104452598317788,4.45218305332902));
#35866=CARTESIAN_POINT('Ctrl Pts',(14.7512124062873,0.178551969979598,4.4283678943965));
#35867=CARTESIAN_POINT('Ctrl Pts',(14.7433410342373,0.242559732875008,4.38839375563686));
#35868=CARTESIAN_POINT('Ctrl Pts',(14.7354696621874,0.30656749577042,4.34841961687722));
#35869=CARTESIAN_POINT('Ctrl Pts',(14.7275982901374,0.360483649899433,4.29228649829047));
#35870=CARTESIAN_POINT('Ctrl Pts',(14.7197269180875,0.397847504376097,4.22672074611392));
#35871=CARTESIAN_POINT('Ctrl Pts',(14.7118555460375,0.435211358852761,4.16115499393738));
#35872=CARTESIAN_POINT('Ctrl Pts',(14.7039841739875,0.456022913677073,4.08615660817103));
#35873=CARTESIAN_POINT('Ctrl Pts',(14.6961128019376,0.457788351878884,4.01071253147039));
#35874=CARTESIAN_POINT('Ctrl Pts',(14.6882414298876,0.459553790080695,3.93526845476975));
#35875=CARTESIAN_POINT('Ctrl Pts',(14.6803700578377,0.442273111660005,3.85937868713481));
#35876=CARTESIAN_POINT('Ctrl Pts',(14.6724986857877,0.408017034045316,3.79213698410258));
#35877=CARTESIAN_POINT('Ctrl Pts',(14.6646273137378,0.373760956430627,3.72489528107034));
#35878=CARTESIAN_POINT('Ctrl Pts',(14.6567559416878,0.32252947962194,3.6663016426408));
#35879=CARTESIAN_POINT('Ctrl Pts',(14.6488845696379,0.260461593653079,3.6233772554918));
#35880=CARTESIAN_POINT('Ctrl Pts',(14.6410131975879,0.198393707684219,3.5804528683428));
#35881=CARTESIAN_POINT('Ctrl Pts',(14.6331418255379,0.125489412555185,3.55319773247434));
#35882=CARTESIAN_POINT('Ctrl Pts',(14.625270453488,0.0504847191830214,3.54487778940425));
#35883=CARTESIAN_POINT('Ctrl Pts',(14.617399081438,-0.0245199741891427,
3.53655784633416));
#35884=CARTESIAN_POINT('Ctrl Pts',(14.6095277093881,-0.101625065804437,
3.54717309606245));
#35885=CARTESIAN_POINT('Ctrl Pts',(14.6016563373381,-0.171591169681571,
3.57545152934398));
#35886=CARTESIAN_POINT('Ctrl Pts',(14.5937849652882,-0.241557273558703,
3.6037299626255));
#35887=CARTESIAN_POINT('Ctrl Pts',(14.5859135932382,-0.304384389697674,
3.64967157946028));
#35888=CARTESIAN_POINT('Ctrl Pts',(14.5780422211883,-0.352544040227279,
3.70777126570269));
#35889=CARTESIAN_POINT('Ctrl Pts',(14.5701708491383,-0.400703690756885,
3.7658709519451));
#35890=CARTESIAN_POINT('Ctrl Pts',(14.5622994770883,-0.434195875677124,
3.83612870759516));
#35891=CARTESIAN_POINT('Ctrl Pts',(14.5544281050384,-0.449007277354457,
3.91012565253846));
#35892=CARTESIAN_POINT('Ctrl Pts',(14.5465567329884,-0.46381867903179,3.98412259748177));
#35893=CARTESIAN_POINT('Ctrl Pts',(14.5386853609385,-0.459949297466218,
4.06185873171832));
#35894=CARTESIAN_POINT('Ctrl Pts',(14.5308139888885,-0.437862794771992,
4.13401905238929));
#35895=CARTESIAN_POINT('Ctrl Pts',(14.5229426168386,-0.415776292077766,
4.20617937306026));
#35896=CARTESIAN_POINT('Ctrl Pts',(14.5150712447886,-0.375472668254887,
4.27276388016565));
#35897=CARTESIAN_POINT('Ctrl Pts',(14.5071998727387,-0.321781445311454,
4.32579385338299));
#35898=CARTESIAN_POINT('Ctrl Pts',(14.4993285006887,-0.26809022236802,4.37882382660034));
#35899=CARTESIAN_POINT('Ctrl Pts',(14.4914571286387,-0.201011400304033,
4.41829926592964));
#35900=CARTESIAN_POINT('Ctrl Pts',(14.4835857565888,-0.128582932452519,
4.43948988945229));
#35901=CARTESIAN_POINT('Ctrl Pts',(14.4790557405542,-0.0868999680795747,
4.45168520479633));
#35902=CARTESIAN_POINT('Ctrl Pts',(14.4745257245197,-0.0434451672832877,
4.45782447382869));
#35903=CARTESIAN_POINT('Ctrl Pts',(14.4699957084852,4.96934848862042E-6,
4.4578413260902));
#35904=CARTESIAN_POINT('Ctrl Pts',(14.5800042915148,-1.58578451148518E-6,
4.45791318879952));
#35905=CARTESIAN_POINT('Ctrl Pts',(14.5801660092442,-0.00155201715944126,
4.45791349841543));
#35906=CARTESIAN_POINT('Ctrl Pts',(14.5803277269736,-0.00310244544229786,
4.45790578589721));
#35907=CARTESIAN_POINT('Ctrl Pts',(14.5804894447029,-0.0046527920161852,
4.45789003224535));
#35908=CARTESIAN_POINT('Ctrl Pts',(14.5883608167529,-0.0801136257596197,
4.45712324646747));
#35909=CARTESIAN_POINT('Ctrl Pts',(14.5962321888029,-0.155380881795201,
4.43730611368561));
#35910=CARTESIAN_POINT('Ctrl Pts',(14.6041035608528,-0.22143539919095,4.4008132908088));
#35911=CARTESIAN_POINT('Ctrl Pts',(14.6119749329028,-0.287489916586699,
4.36432046793199));
#35912=CARTESIAN_POINT('Ctrl Pts',(14.6198463049527,-0.344331695342615,
4.31115195496024));
#35913=CARTESIAN_POINT('Ctrl Pts',(14.6277176770027,-0.38514947146564,4.24767885402976));
#35914=CARTESIAN_POINT('Ctrl Pts',(14.6355890490526,-0.425967247588666,
4.18420575309928));
#35915=CARTESIAN_POINT('Ctrl Pts',(14.6434604211026,-0.4507610210788,4.11042806421008));
#35916=CARTESIAN_POINT('Ctrl Pts',(14.6513317931525,-0.45655979174196,4.03518645571321));
#35917=CARTESIAN_POINT('Ctrl Pts',(14.6592031652025,-0.462358562405121,
3.95994484721634));
#35918=CARTESIAN_POINT('Ctrl Pts',(14.6670745372524,-0.449162330241309,
3.8832393191118));
#35919=CARTESIAN_POINT('Ctrl Pts',(14.6749459093024,-0.41855237967279,3.81426137832517));
#35920=CARTESIAN_POINT('Ctrl Pts',(14.6828172813524,-0.387942429104271,
3.74528343753854));
#35921=CARTESIAN_POINT('Ctrl Pts',(14.6906886534023,-0.339918760131043,
3.68403308406983));
#35922=CARTESIAN_POINT('Ctrl Pts',(14.6985600254523,-0.280235976103336,
3.63784985464301));
#35923=CARTESIAN_POINT('Ctrl Pts',(14.7064313975022,-0.220553192075631,
3.5916666252162));
#35924=CARTESIAN_POINT('Ctrl Pts',(14.7143027695522,-0.149211292993445,
3.5605505198313));
#35925=CARTESIAN_POINT('Ctrl Pts',(14.7221741416021,-0.0747590701011626,
3.54823013427646));
#35926=CARTESIAN_POINT('Ctrl Pts',(14.7300455136521,-0.000306847208877067,
3.53590974872161));
#35927=CARTESIAN_POINT('Ctrl Pts',(14.737916885702,0.0772556994935079,3.54238508299684));
#35928=CARTESIAN_POINT('Ctrl Pts',(14.745788257752,0.148634367597872,3.5668802073009));
#35929=CARTESIAN_POINT('Ctrl Pts',(14.753659629802,0.220013035702235,3.59137533160497));
#35930=CARTESIAN_POINT('Ctrl Pts',(14.7615310018519,0.285207825208577,3.63389024593787));
#35931=CARTESIAN_POINT('Ctrl Pts',(14.7694023739019,0.336406544142474,3.68933045342307));
#35932=CARTESIAN_POINT('Ctrl Pts',(14.7772737459518,0.387605263076371,3.74477066090827));
#35933=CARTESIAN_POINT('Ctrl Pts',(14.7851451180018,0.424807911437823,3.81313616154577));
#35934=CARTESIAN_POINT('Ctrl Pts',(14.7930164900517,0.443556551112275,3.88623481973509));
#35935=CARTESIAN_POINT('Ctrl Pts',(14.8008878621017,0.462305190786727,3.9593334779244));
#35936=CARTESIAN_POINT('Ctrl Pts',(14.8087592341516,0.462599821774179,4.03716529366552));
#35937=CARTESIAN_POINT('Ctrl Pts',(14.8166306062016,0.444405141642572,4.11040380200553));
#35938=CARTESIAN_POINT('Ctrl Pts',(14.8245019782516,0.426210461510966,4.18364231034555));
#35939=CARTESIAN_POINT('Ctrl Pts',(14.8323733503015,0.389526470260302,4.25228751128446));
#35940=CARTESIAN_POINT('Ctrl Pts',(14.8402447223515,0.338748948932789,4.3081137476731));
#35941=CARTESIAN_POINT('Ctrl Pts',(14.8481160944014,0.287971427605278,4.36393998406173));
#35942=CARTESIAN_POINT('Ctrl Pts',(14.8559874664514,0.22310037620092,4.40694725590009));
#35943=CARTESIAN_POINT('Ctrl Pts',(14.8638588385013,0.151909206873508,4.43198208217373));
#35944=CARTESIAN_POINT('Ctrl Pts',(14.8692406561725,0.103234351881841,4.44909890368578));
#35945=CARTESIAN_POINT('Ctrl Pts',(14.8746224738437,0.0516050086776526,
4.45781408155485));
#35946=CARTESIAN_POINT('Ctrl Pts',(14.8800042915148,-1.01702808208336E-5,
4.45785711824254));
#35947=CARTESIAN_POINT('Origin',(12.5,0.,4.));
#35948=CARTESIAN_POINT('',(15.1,-5.60735153159594E-17,4.457875));
#35949=CARTESIAN_POINT('',(15.0699957084852,-1.05870731373636E-5,4.45788944868556));
#35950=CARTESIAN_POINT('',(12.5,-5.60735153159594E-17,4.457875));
#35951=CARTESIAN_POINT('',(15.1,-0.269165465906718,4.37040446485999));
#35952=CARTESIAN_POINT('Origin',(15.1,0.,4.));
#35953=CARTESIAN_POINT('Ctrl Pts',(15.1,-0.269173508333955,4.37043259773194));
#35954=CARTESIAN_POINT('Ctrl Pts',(15.0991842588284,-0.262849866117432,
4.37503549456412));
#35955=CARTESIAN_POINT('Ctrl Pts',(15.0983685176569,-0.256407545646713,
4.37947450812006));
#35956=CARTESIAN_POINT('Ctrl Pts',(15.0975527764853,-0.249853611926923,
4.38374199825787));
#35957=CARTESIAN_POINT('Ctrl Pts',(15.0896814044354,-0.186612411779406,
4.42492050409441));
#35958=CARTESIAN_POINT('Ctrl Pts',(15.0818100323854,-0.112978907049287,
4.45012847221118));
#35959=CARTESIAN_POINT('Ctrl Pts',(15.0739386603355,-0.0377721395608013,
4.45635245505497));
#35960=CARTESIAN_POINT('Ctrl Pts',(15.072624343052,-0.0252145379490987,
4.45739170058566));
#35961=CARTESIAN_POINT('Ctrl Pts',(15.0713100257686,-0.0126130730861363,
4.45790166433459));
#35962=CARTESIAN_POINT('Ctrl Pts',(15.0699957084852,-1.05870731373636E-5,
4.45788944868556));
#35963=CARTESIAN_POINT('Origin',(11.8752146997001,0.,4.));
#35964=CARTESIAN_POINT('',(14.9247853002999,-1.38824472118437E-5,4.62497559137666));
#35965=CARTESIAN_POINT('',(15.0252146997001,-1.44513692928093E-5,4.62501972247551));
#35966=CARTESIAN_POINT('',(11.8752146997001,-1.68747709936658E-14,4.625));
#35967=CARTESIAN_POINT('',(15.1,-0.624993681275899,4.00281040303151));
#35968=CARTESIAN_POINT('Ctrl Pts',(15.0252146997001,-1.44513692928189E-5,
4.62501972247551));
#35969=CARTESIAN_POINT('Ctrl Pts',(15.0265290169835,-0.017216861979444,
4.62503639685311));
#35970=CARTESIAN_POINT('Ctrl Pts',(15.0357147063169,-0.137433797398843,
4.62017138475037));
#35971=CARTESIAN_POINT('Ctrl Pts',(15.0527717677003,-0.355236031271534,
4.54560815721762));
#35972=CARTESIAN_POINT('Ctrl Pts',(15.0763858838501,-0.571652475026301,
4.31158258982903));
#35973=CARTESIAN_POINT('Ctrl Pts',(15.09212862795,-0.624530364890795,4.10584538053252));
#35974=CARTESIAN_POINT('Ctrl Pts',(15.1,-0.624993681275899,4.00281040303152));
#35975=CARTESIAN_POINT('',(15.1,0.314930721058197,3.46014479632612));
#35976=CARTESIAN_POINT('Origin',(15.1,0.,4.));
#35977=CARTESIAN_POINT('Ctrl Pts',(14.9247853002999,-1.38824472118368E-5,
4.62497559137666));
#35978=CARTESIAN_POINT('Ctrl Pts',(14.9272748546787,-0.0326052931943186,
4.62500276606431));
#35979=CARTESIAN_POINT('Ctrl Pts',(14.9376357811074,-0.168225686180582,
4.61457389311938));
#35980=CARTESIAN_POINT('Ctrl Pts',(14.9558680795861,-0.394527586443172,
4.517903766532));
#35981=CARTESIAN_POINT('Ctrl Pts',(14.979482195736,-0.593077772790822,4.26857965265179));
#35982=CARTESIAN_POINT('Ctrl Pts',(15.0030963118859,-0.649493436571599,
3.95488773069898));
#35983=CARTESIAN_POINT('Ctrl Pts',(15.0267104280357,-0.550252000240565,
3.65200904506483));
#35984=CARTESIAN_POINT('Ctrl Pts',(15.0503245441856,-0.319142060764588,
3.43252503194012));
#35985=CARTESIAN_POINT('Ctrl Pts',(15.0739386603355,-0.0115409051696555,
3.34904846156061));
#35986=CARTESIAN_POINT('Ctrl Pts',(15.0904971456069,0.20608092381284,3.39989411918499));
#35987=CARTESIAN_POINT('Ctrl Pts',(15.0991842588284,0.305720220830039,3.45471854406458));
#35988=CARTESIAN_POINT('Ctrl Pts',(15.1,0.314937815442301,3.46010549098218));
#35989=CARTESIAN_POINT('Origin',(11.8752146997001,0.,4.));
#35990=CARTESIAN_POINT('',(14.6247853002999,-2.16459804047719E-6,4.62505212776347));
#35991=CARTESIAN_POINT('',(14.7252146997001,1.17863019661874E-5,4.62503218402409));
#35992=CARTESIAN_POINT('',(11.8752146997001,-1.68747709936658E-14,4.625));
#35993=CARTESIAN_POINT('Ctrl Pts',(14.7252146997001,1.17863019662174E-5,
4.62503218402409));
#35994=CARTESIAN_POINT('Ctrl Pts',(14.7320725523841,-0.0897427467603322,
4.62495430540108));
#35995=CARTESIAN_POINT('Ctrl Pts',(14.746801777118,-0.282587126126967,4.58296482291278));
#35996=CARTESIAN_POINT('Ctrl Pts',(14.7694023739019,-0.520130285395982,
4.39158760667368));
#35997=CARTESIAN_POINT('Ctrl Pts',(14.7930164900517,-0.64367318065081,4.09778141619902));
#35998=CARTESIAN_POINT('Ctrl Pts',(14.8166306062016,-0.612955311082805,
3.78054123783642));
#35999=CARTESIAN_POINT('Ctrl Pts',(14.8402447223515,-0.435338447621071,
3.51589585985611));
#36000=CARTESIAN_POINT('Ctrl Pts',(14.8638588385013,-0.153389665944836,
3.36726945127358));
#36001=CARTESIAN_POINT('Ctrl Pts',(14.8874729546512,0.165319955489652,3.37028123293502));
#36002=CARTESIAN_POINT('Ctrl Pts',(14.9110870708011,0.444409630539555,3.52420969451069));
#36003=CARTESIAN_POINT('Ctrl Pts',(14.9347011869509,0.616993161964042,3.79216419995926));
#36004=CARTESIAN_POINT('Ctrl Pts',(14.9583153031008,0.641710593195818,4.10992889087348));
#36005=CARTESIAN_POINT('Ctrl Pts',(14.9819294192507,0.512636325700993,4.40134645341462));
#36006=CARTESIAN_POINT('Ctrl Pts',(15.0042292181171,0.274729866520086,4.58571614948967));
#36007=CARTESIAN_POINT('Ctrl Pts',(15.0186576449336,0.0858074045169303,
4.62493653494651));
#36008=CARTESIAN_POINT('Ctrl Pts',(15.0252146997001,-1.44513692928189E-5,
4.62501972247551));
#36009=CARTESIAN_POINT('Ctrl Pts',(14.6247853002999,-2.16459804049194E-6,
4.62505212776347));
#36010=CARTESIAN_POINT('Ctrl Pts',(14.6249470180292,-0.00211850554115318,
4.62505255038961));
#36011=CARTESIAN_POINT('Ctrl Pts',(14.6329801078086,-0.107244412024774,
4.62452960748548));
#36012=CARTESIAN_POINT('Ctrl Pts',(14.6488845696379,-0.314835022974042,
4.56987302880665));
#36013=CARTESIAN_POINT('Ctrl Pts',(14.6724986857877,-0.547602339746838,
4.35214775046202));
#36014=CARTESIAN_POINT('Ctrl Pts',(14.6961128019376,-0.649132943719538,
4.05002781234082));
#36015=CARTESIAN_POINT('Ctrl Pts',(14.7197269180875,-0.595094318970103,
3.73591836064326));
#36016=CARTESIAN_POINT('Ctrl Pts',(14.7433410342373,-0.398437197867616,
3.48509791236843));
#36017=CARTESIAN_POINT('Ctrl Pts',(14.7669551503872,-0.1062918289807,3.35767733339665));
#36018=CARTESIAN_POINT('Ctrl Pts',(14.7905692665371,0.211327117384507,3.38419385377023));
#36019=CARTESIAN_POINT('Ctrl Pts',(14.8141833826869,0.478300047385911,3.5582926020622));
#36020=CARTESIAN_POINT('Ctrl Pts',(14.8377974988368,0.630645044771057,3.83824960712979));
#36021=CARTESIAN_POINT('Ctrl Pts',(14.8614116149867,0.631851559871185,4.15697121131127));
#36022=CARTESIAN_POINT('Ctrl Pts',(14.8850257311365,0.481630465478622,4.4380735902585));
#36023=CARTESIAN_POINT('Ctrl Pts',(14.9061502929076,0.243989509668873,4.59562135563586));
#36024=CARTESIAN_POINT('Ctrl Pts',(14.9194034826287,0.0704409072858971,
4.62491684623921));
#36025=CARTESIAN_POINT('Ctrl Pts',(14.9247853002999,-1.38824472118368E-5,
4.62497559137666));
#36026=CARTESIAN_POINT('Origin',(11.8752146997001,0.,4.));
#36027=CARTESIAN_POINT('',(14.3247853002999,1.51969053300144E-5,4.6249871875462));
#36028=CARTESIAN_POINT('',(14.4252146997001,6.78316748347314E-6,4.62495403506715));
#36029=CARTESIAN_POINT('',(11.8752146997001,-1.68747709936658E-14,4.625));
#36030=CARTESIAN_POINT('Ctrl Pts',(14.4252146997001,6.78316748347826E-6,
4.62495403506715));
#36031=CARTESIAN_POINT('Ctrl Pts',(14.4297447157347,-0.0593027126443913,
4.62493103170719));
#36032=CARTESIAN_POINT('Ctrl Pts',(14.4421461038192,-0.221686029527806,
4.60198961095629));
#36033=CARTESIAN_POINT('Ctrl Pts',(14.4624188639536,-0.457506203155893,
4.46321101183598));
#36034=CARTESIAN_POINT('Ctrl Pts',(14.4860329801035,-0.622549707754089,
4.19054718257559));
#36035=CARTESIAN_POINT('Ctrl Pts',(14.5096470962533,-0.63839484111024,3.87221739454711));
#36036=CARTESIAN_POINT('Ctrl Pts',(14.5332612124032,-0.501244206711231,
3.58451159745434));
#36037=CARTESIAN_POINT('Ctrl Pts',(14.5568753285531,-0.243966908844842,
3.39638048838484));
#36038=CARTESIAN_POINT('Ctrl Pts',(14.5804894447029,0.0717787570654544,
3.35291099727801));
#36039=CARTESIAN_POINT('Ctrl Pts',(14.6041035608528,0.370322144162233,3.46452089026927));
#36040=CARTESIAN_POINT('Ctrl Pts',(14.6277176770027,0.580115251486915,3.70446207957941));
#36041=CARTESIAN_POINT('Ctrl Pts',(14.6513317931525,0.650879700384091,4.0152309888134));
#36042=CARTESIAN_POINT('Ctrl Pts',(14.6749459093024,0.565656298155129,4.32234968564526));
#36043=CARTESIAN_POINT('Ctrl Pts',(14.6985600254523,0.344869426209941,4.55221503612336));
#36044=CARTESIAN_POINT('Ctrl Pts',(14.7153162889182,0.129554394067723,4.62141618582314));
#36045=CARTESIAN_POINT('Ctrl Pts',(14.7242011803341,0.0132765736394338,
4.62504369367533));
#36046=CARTESIAN_POINT('Ctrl Pts',(14.7252146997001,1.17863019662174E-5,
4.62503218402409));
#36047=CARTESIAN_POINT('Ctrl Pts',(14.3247853002999,1.51969053300109E-5,
4.6249871875462));
#36048=CARTESIAN_POINT('Ctrl Pts',(14.3304905534298,-0.0746697890657793,
4.62491698721088));
#36049=CARTESIAN_POINT('Ctrl Pts',(14.3440671786096,-0.252453835406249,
4.59302599116618));
#36050=CARTESIAN_POINT('Ctrl Pts',(14.3655151758395,-0.490432948250941,
4.42819608115853));
#36051=CARTESIAN_POINT('Ctrl Pts',(14.3891292919893,-0.634910852255616,
4.14409916841427));
#36052=CARTESIAN_POINT('Ctrl Pts',(14.4127434081392,-0.627227950688033,
3.82546788683648));
#36053=CARTESIAN_POINT('Ctrl Pts',(14.4363575242891,-0.469225504392149,
3.54866444115539));
#36054=CARTESIAN_POINT('Ctrl Pts',(14.4599716404389,-0.198769899531221,
3.38002670405092));
#36055=CARTESIAN_POINT('Ctrl Pts',(14.4835857565888,0.11932229545683,3.35996988316441));
#36056=CARTESIAN_POINT('Ctrl Pts',(14.5071998727387,0.408818071695872,3.49330073524378));
#36057=CARTESIAN_POINT('Ctrl Pts',(14.5308139888885,0.600337751131954,3.74806559342675));
#36058=CARTESIAN_POINT('Ctrl Pts',(14.5544281050384,0.647982309355475,4.06320828594604));
#36059=CARTESIAN_POINT('Ctrl Pts',(14.5780422211883,0.540333396317157,4.36320267272319));
#36060=CARTESIAN_POINT('Ctrl Pts',(14.6014946196088,0.304813865567294,4.57469465218781));
#36061=CARTESIAN_POINT('Ctrl Pts',(14.6170756459793,0.100891269655612,4.62503197968527));
#36062=CARTESIAN_POINT('Ctrl Pts',(14.6247853002999,-2.16459804049194E-6,
4.62505212776347));
#36063=CARTESIAN_POINT('Origin',(11.8752146997001,0.,4.));
#36064=CARTESIAN_POINT('',(14.0247853002999,-6.3966029390794E-6,4.62495348172753));
#36065=CARTESIAN_POINT('',(14.1252146997001,-1.50974863142078E-5,4.62498583382255));
#36066=CARTESIAN_POINT('',(11.8752146997001,-1.68747709936658E-14,4.625));
#36067=CARTESIAN_POINT('Ctrl Pts',(14.1252146997001,-1.50974863141889E-5,
4.62498583382255));
#36068=CARTESIAN_POINT('Ctrl Pts',(14.1274168790852,-0.0288430498503269,
4.62501265364587));
#36069=CARTESIAN_POINT('Ctrl Pts',(14.1374904305203,-0.160695812902997,
4.61605202430223));
#36070=CARTESIAN_POINT('Ctrl Pts',(14.1554353540053,-0.385112282251534,
4.52494275637564));
#36071=CARTESIAN_POINT('Ctrl Pts',(14.1790494701552,-0.588131968915973,
4.27924389796604));
#36072=CARTESIAN_POINT('Ctrl Pts',(14.2026635863051,-0.65020173504413,3.96662229549764));
#36073=CARTESIAN_POINT('Ctrl Pts',(14.2262777024549,-0.556446129094758,
3.66199989226673));
#36074=CARTESIAN_POINT('Ctrl Pts',(14.2498918186048,-0.329334334698108,
3.43838156778717));
#36075=CARTESIAN_POINT('Ctrl Pts',(14.2735059347547,-0.0232952743833569,
3.34935901020328));
#36076=CARTESIAN_POINT('Ctrl Pts',(14.2971200509045,0.28832666060365,3.41626709515619));
#36077=CARTESIAN_POINT('Ctrl Pts',(14.3207341670544,0.530849104237583,3.62307083431711));
#36078=CARTESIAN_POINT('Ctrl Pts',(14.3443482832043,0.646149864620809,3.92020827196535));
#36079=CARTESIAN_POINT('Ctrl Pts',(14.3679623993541,0.606596311879891,4.2364683526943));
#36080=CARTESIAN_POINT('Ctrl Pts',(14.391576515504,0.42166773027486,4.49605714656388));
#36081=CARTESIAN_POINT('Ctrl Pts',(14.4106606156193,0.190545343529355,4.60977018898031));
#36082=CARTESIAN_POINT('Ctrl Pts',(14.4218733436847,0.0437536792250838,
4.62497100242767));
#36083=CARTESIAN_POINT('Ctrl Pts',(14.4252146997001,6.78316748347826E-6,
4.62495403506715));
#36084=CARTESIAN_POINT('Ctrl Pts',(14.0247853002999,-6.39660293913491E-6,
4.62495348172753));
#36085=CARTESIAN_POINT('Ctrl Pts',(14.0281627167804,-0.0442255271350925,
4.62496963662755));
#36086=CARTESIAN_POINT('Ctrl Pts',(14.0394115053108,-0.191490205391595,
4.6095527480466));
#36087=CARTESIAN_POINT('Ctrl Pts',(14.0585316658912,-0.422790583021024,
4.49510047824495));
#36088=CARTESIAN_POINT('Ctrl Pts',(14.0821457820411,-0.60713052675338,4.23509335195577));
#36089=CARTESIAN_POINT('Ctrl Pts',(14.1057598981909,-0.645967413308333,
3.91874446730605));
#36090=CARTESIAN_POINT('Ctrl Pts',(14.1293740143408,-0.529993712466286,
3.62186903671368));
#36091=CARTESIAN_POINT('Ctrl Pts',(14.1529881304907,-0.287003328966194,
3.41561532377041));
#36092=CARTESIAN_POINT('Ctrl Pts',(14.1766022466405,0.0247694002478971,
3.34941346658496));
#36093=CARTESIAN_POINT('Ctrl Pts',(14.2002163627904,0.330605970264406,3.43912920108534));
#36094=CARTESIAN_POINT('Ctrl Pts',(14.2238304789403,0.557210518047066,3.66326152695696));
#36095=CARTESIAN_POINT('Ctrl Pts',(14.2474445950901,0.650275686248857,3.96809557204375));
#36096=CARTESIAN_POINT('Ctrl Pts',(14.27105871124,0.587497759452106,4.28057573538778));
#36097=CARTESIAN_POINT('Ctrl Pts',(14.2946728273899,0.383921904832036,4.52581397056352));
#36098=CARTESIAN_POINT('Ctrl Pts',(14.3125816904098,0.159750963363977,4.61623247111552));
#36099=CARTESIAN_POINT('Ctrl Pts',(14.3226191813798,0.0283709170587055,
4.62501384057475));
#36100=CARTESIAN_POINT('Ctrl Pts',(14.3247853002999,1.51969053300109E-5,
4.6249871875462));
#36101=CARTESIAN_POINT('Origin',(11.8752146997001,0.,4.));
#36102=CARTESIAN_POINT('',(13.7247853002999,-1.20831421157597E-5,4.62503091248755));
#36103=CARTESIAN_POINT('',(13.8252146997001,1.68461488569462E-6,4.62505238998457));
#36104=CARTESIAN_POINT('',(11.8752146997001,-1.68747709936658E-14,4.625));
#36105=CARTESIAN_POINT('Ctrl Pts',(13.8252146997001,1.68461488569581E-6,
4.62505238998457));
#36106=CARTESIAN_POINT('Ctrl Pts',(13.8329604144858,-0.101363538932993,
4.62503644193381));
#36107=CARTESIAN_POINT('Ctrl Pts',(13.8485775013214,-0.305753798836605,
4.57432856173903));
#36108=CARTESIAN_POINT('Ctrl Pts',(13.8720659602069,-0.541154937947787,
4.36197748624323));
#36109=CARTESIAN_POINT('Ctrl Pts',(13.8956800763568,-0.648123865072376,
4.06173996222779));
#36110=CARTESIAN_POINT('Ctrl Pts',(13.9192941925067,-0.599765396122921,
3.74670602647169));
#36111=CARTESIAN_POINT('Ctrl Pts',(13.9429083086565,-0.407668974822819,
3.49237575473668));
#36112=CARTESIAN_POINT('Ctrl Pts',(13.9665224248064,-0.117871845784803,
3.35970116712309));
#36113=CARTESIAN_POINT('Ctrl Pts',(13.9901365409563,0.200174091641329,3.38047865214521));
#36114=CARTESIAN_POINT('Ctrl Pts',(14.0137506571061,0.470246914526057,3.54972874087838));
#36115=CARTESIAN_POINT('Ctrl Pts',(14.037364773256,0.627621790796785,3.82688947135059));
#36116=CARTESIAN_POINT('Ctrl Pts',(14.0609788894059,0.634582735815489,4.14553734509456));
#36117=CARTESIAN_POINT('Ctrl Pts',(14.0845930055557,0.489461510650943,4.42930618095194));
#36118=CARTESIAN_POINT('Ctrl Pts',(14.1060049423205,0.251510284961593,4.59332024860173));
#36119=CARTESIAN_POINT('Ctrl Pts',(14.1195455070353,0.074198300926532,4.62491679006221));
#36120=CARTESIAN_POINT('Ctrl Pts',(14.1252146997001,-1.50974863141889E-5,
4.62498583382255));
#36121=CARTESIAN_POINT('Ctrl Pts',(13.7247853002999,-1.20831421156938E-5,
4.62503091248755));
#36122=CARTESIAN_POINT('Ctrl Pts',(13.7258348801309,-0.013748904810447,
4.62504304225186));
#36123=CARTESIAN_POINT('Ctrl Pts',(13.734755832012,-0.130498998332177,4.62127102305724));
#36124=CARTESIAN_POINT('Ctrl Pts',(13.7515481559429,-0.346119716157775,
4.55143222859795));
#36125=CARTESIAN_POINT('Ctrl Pts',(13.7751622720928,-0.566385203513325,
4.32106722332061));
#36126=CARTESIAN_POINT('Ctrl Pts',(13.7987763882427,-0.650912534047929,
4.01375622291695));
#36127=CARTESIAN_POINT('Ctrl Pts',(13.8223905043925,-0.57944414457563,3.70314844792952));
#36128=CARTESIAN_POINT('Ctrl Pts',(13.8460046205424,-0.369107932149097,
3.46368321387984));
#36129=CARTESIAN_POINT('Ctrl Pts',(13.8696187366923,-0.0703124342978696,
3.35275003110641));
#36130=CARTESIAN_POINT('Ctrl Pts',(13.8932328528421,0.245333927901481,3.3969348091043));
#36131=CARTESIAN_POINT('Ctrl Pts',(13.916846968992,0.502184306426786,3.58564835824111));
#36132=CARTESIAN_POINT('Ctrl Pts',(13.9404610851419,0.638682720042094,3.87366416276737));
#36133=CARTESIAN_POINT('Ctrl Pts',(13.9640752012917,0.62211637371287,4.19195723015293));
#36134=CARTESIAN_POINT('Ctrl Pts',(13.9876893174416,0.456455507660852,4.46424641105313));
#36135=CARTESIAN_POINT('Ctrl Pts',(14.007926017111,0.220741531225703,4.60224444133776));
#36136=CARTESIAN_POINT('Ctrl Pts',(14.0202913447304,0.058831122868106,4.62493198618401));
#36137=CARTESIAN_POINT('Ctrl Pts',(14.0247853002999,-6.39660293913491E-6,
4.62495348172753));
#36138=CARTESIAN_POINT('Origin',(11.8752146997001,0.,4.));
#36139=CARTESIAN_POINT('',(13.4247853002999,1.36962628664028E-5,4.62502243215823));
#36140=CARTESIAN_POINT('',(13.5252146997001,1.40828270379035E-5,4.62497680637469));
#36141=CARTESIAN_POINT('',(11.8752146997001,-1.68747709936658E-14,4.625));
#36142=CARTESIAN_POINT('Ctrl Pts',(13.5252146997001,1.4082827037902E-5,
4.62497680637469));
#36143=CARTESIAN_POINT('Ctrl Pts',(13.5306325778363,-0.0709123884867814,
4.62491668074428));
#36144=CARTESIAN_POINT('Ctrl Pts',(13.5439218280225,-0.244933372371362,
4.59533688876844));
#36145=CARTESIAN_POINT('Ctrl Pts',(13.5650824502587,-0.482621788093898,
4.43698120905743));
#36146=CARTESIAN_POINT('Ctrl Pts',(13.5886965664085,-0.632205603168059,
4.15553919999523));
#36147=CARTESIAN_POINT('Ctrl Pts',(13.6123106825584,-0.630276944445953,
3.83682113889318));
#36148=CARTESIAN_POINT('Ctrl Pts',(13.6359247987083,-0.477298028416376,
3.55721002779864));
#36149=CARTESIAN_POINT('Ctrl Pts',(13.6595389148582,-0.209931317243796,
3.38371661595291));
#36150=CARTESIAN_POINT('Ctrl Pts',(13.683153031008,0.107746895509167,3.35791980725116));
#36151=CARTESIAN_POINT('Ctrl Pts',(13.7067671471579,0.399602814690774,3.48600198647908));
#36152=CARTESIAN_POINT('Ctrl Pts',(13.7303812633077,0.59569113756138,3.73726736776131));
#36153=CARTESIAN_POINT('Ctrl Pts',(13.7539953794576,0.649017932507905,4.05149845333026));
#36154=CARTESIAN_POINT('Ctrl Pts',(13.7776094956075,0.546803061895555,4.35338757606046));
#36155=CARTESIAN_POINT('Ctrl Pts',(13.8012236117573,0.313543031018869,4.57058490613733));
#36156=CARTESIAN_POINT('Ctrl Pts',(13.8170920131216,0.106300066848774,4.6246481407235));
#36157=CARTESIAN_POINT('Ctrl Pts',(13.8250890424358,0.00164611344283092,
4.62505264870678));
#36158=CARTESIAN_POINT('Ctrl Pts',(13.8252146997001,1.68461488569581E-6,
4.62505238998457));
#36159=CARTESIAN_POINT('Ctrl Pts',(13.4247853002999,1.36962628664097E-5,
4.62502243215823));
#36160=CARTESIAN_POINT('Ctrl Pts',(13.4313784155315,-0.086279884022628,
4.62493973056585));
#36161=CARTESIAN_POINT('Ctrl Pts',(13.445842902813,-0.275670893367246,4.58538934244717));
#36162=CARTESIAN_POINT('Ctrl Pts',(13.4681787621445,-0.513544980480383,
4.40018484937968));
#36163=CARTESIAN_POINT('Ctrl Pts',(13.4917928782944,-0.64195771209056,4.10847422061066));
#36164=CARTESIAN_POINT('Ctrl Pts',(13.5154069944443,-0.616520809113462,
3.79076698974655));
#36165=CARTESIAN_POINT('Ctrl Pts',(13.5390211105941,-0.443330402422436,
3.52320390633144));
#36166=CARTESIAN_POINT('Ctrl Pts',(13.562635226744,-0.163892778617988,3.36990832590288));
#36167=CARTESIAN_POINT('Ctrl Pts',(13.5862493428939,0.154822890495328,3.36761860145296));
#36168=CARTESIAN_POINT('Ctrl Pts',(13.6098634590437,0.43643417612693,3.51688348138565));
#36169=CARTESIAN_POINT('Ctrl Pts',(13.6334775751936,0.613450973283793,3.78193059814177));
#36170=CARTESIAN_POINT('Ctrl Pts',(13.6570916913435,0.643449974253473,4.09923956510808));
#36171=CARTESIAN_POINT('Ctrl Pts',(13.6807058074933,0.519241709620395,4.39276507945606));
#36172=CARTESIAN_POINT('Ctrl Pts',(13.7032703438121,0.281645253009076,4.58329909926801));
#36173=CARTESIAN_POINT('Ctrl Pts',(13.717963508081,0.0892710189108511,4.62495207452848));
#36174=CARTESIAN_POINT('Ctrl Pts',(13.7247853002999,-1.20831421156938E-5,
4.62503091248755));
#36175=CARTESIAN_POINT('Origin',(11.8752146997001,0.,4.));
#36176=CARTESIAN_POINT('',(13.1247853002999,3.84888821539087E-6,4.62495078081483));
#36177=CARTESIAN_POINT('',(13.2252146997001,-9.32440196476731E-6,4.62495874418382));
#36178=CARTESIAN_POINT('',(11.8752146997001,-1.68747709936658E-14,4.625));
#36179=CARTESIAN_POINT('Ctrl Pts',(13.2252146997001,-9.32440196474427E-6,
4.62495874418382));
#36180=CARTESIAN_POINT('Ctrl Pts',(13.2283047411869,-0.040464997295585,
4.62498052751194));
#36181=CARTESIAN_POINT('Ctrl Pts',(13.2392661547237,-0.18396024524725,4.61125364372682));
#36182=CARTESIAN_POINT('Ctrl Pts',(13.2580989403104,-0.413782468289504,
4.50265339583901));
#36183=CARTESIAN_POINT('Ctrl Pts',(13.2817130564603,-0.602786876612853,
4.24601696851145));
#36184=CARTESIAN_POINT('Ctrl Pts',(13.3053271726101,-0.647329213752593,
3.9304208620728));
#36185=CARTESIAN_POINT('Ctrl Pts',(13.32894128876,-0.536734598538914,3.6314998804023));
#36186=CARTESIAN_POINT('Ctrl Pts',(13.3525554049099,-0.297507800394296,
3.42089251764738));
#36187=CARTESIAN_POINT('Ctrl Pts',(13.3761695210598,0.0130188131672444,
3.34907229440132));
#36188=CARTESIAN_POINT('Ctrl Pts',(13.3997836372096,0.320425377524893,3.43325142712992));
#36189=CARTESIAN_POINT('Ctrl Pts',(13.4233977533595,0.551039769569266,3.65325580067535));
#36190=CARTESIAN_POINT('Ctrl Pts',(13.4470118695093,0.649593644862141,3.95635983539258));
#36191=CARTESIAN_POINT('Ctrl Pts',(13.4706259856592,0.592467881122722,4.26992253935193));
#36192=CARTESIAN_POINT('Ctrl Pts',(13.4942401018091,0.393353065302923,4.5187964277335));
#36193=CARTESIAN_POINT('Ctrl Pts',(13.5124363398227,0.1672808180195,4.61476328251587));
#36194=CARTESIAN_POINT('Ctrl Pts',(13.5227612057864,0.0321332374692893,
4.62500403435298));
#36195=CARTESIAN_POINT('Ctrl Pts',(13.5252146997001,1.4082827037902E-5,
4.62497680637469));
#36196=CARTESIAN_POINT('Ctrl Pts',(13.1247853002999,3.84888821536311E-6,
4.62495078081483));
#36197=CARTESIAN_POINT('Ctrl Pts',(13.1290505788821,-0.0558403875021823,
4.6249385719914));
#36198=CARTESIAN_POINT('Ctrl Pts',(13.1411872295142,-0.214751600407627,
4.60383286368317));
#36199=CARTESIAN_POINT('Ctrl Pts',(13.1611952521963,-0.449738236712957,
4.47075670902068));
#36200=CARTESIAN_POINT('Ctrl Pts',(13.1848093683461,-0.619294173608025,
4.2008758003961));
#36201=CARTESIAN_POINT('Ctrl Pts',(13.208423484496,-0.64043195068177,3.88285360784221));
#36202=CARTESIAN_POINT('Ctrl Pts',(13.2320376006459,-0.508085752511173,
3.59290636366459));
#36203=CARTESIAN_POINT('Ctrl Pts',(13.2556517167957,-0.253973266794505,
3.40052194335125));
#36204=CARTESIAN_POINT('Ctrl Pts',(13.2792658329456,0.0610056803032868,
3.3518066124833));
#36205=CARTESIAN_POINT('Ctrl Pts',(13.3028799490955,0.361364191435218,3.45843533922715));
#36206=CARTESIAN_POINT('Ctrl Pts',(13.3264940652453,0.575119258511334,3.69485380694));
#36207=CARTESIAN_POINT('Ctrl Pts',(13.3501081813952,0.65104299168552,4.00440268404554));
#36208=CARTESIAN_POINT('Ctrl Pts',(13.3737222975451,0.570939739771795,4.31289642727099));
#36209=CARTESIAN_POINT('Ctrl Pts',(13.3973364136949,0.354006804717113,4.54640236352309));
#36210=CARTESIAN_POINT('Ctrl Pts',(13.4143574146132,0.136489422610972,4.62032507485564));
#36211=CARTESIAN_POINT('Ctrl Pts',(13.4235070434815,0.0167440814458925,
4.62503846613771));
#36212=CARTESIAN_POINT('Ctrl Pts',(13.4247853002999,1.36962628664097E-5,
4.62502243215823));
#36213=CARTESIAN_POINT('Origin',(11.8752146997001,0.,4.));
#36214=CARTESIAN_POINT('',(12.8247853002999,-1.55438223423121E-5,4.62499607812274));
#36215=CARTESIAN_POINT('',(12.9252146997001,-9.4222586321007E-6,4.62504029123831));
#36216=CARTESIAN_POINT('',(11.8752146997001,-1.68747709936658E-14,4.625));
#36217=CARTESIAN_POINT('Ctrl Pts',(12.9252146997001,-9.42225863212465E-6,
4.62504029123832));
#36218=CARTESIAN_POINT('Ctrl Pts',(12.9259769045375,-0.00998466834883174,
4.6250476064301));
#36219=CARTESIAN_POINT('Ctrl Pts',(12.9346104814248,-0.122971475467856,
4.62239759066569));
#36220=CARTESIAN_POINT('Ctrl Pts',(12.9511154303622,-0.336107011072318,
4.55759164674784));
#36221=CARTESIAN_POINT('Ctrl Pts',(12.974729546512,-0.56049590900091,4.33124115596169));
#36222=CARTESIAN_POINT('Ctrl Pts',(12.9983436626619,-0.650558060547343,
4.02550641626558));
#36223=CARTESIAN_POINT('Ctrl Pts',(13.0219577788117,-0.584709444123524,
3.71365888635357));
#36224=CARTESIAN_POINT('Ctrl Pts',(13.0455718949616,-0.378731139057797,
3.47043499764384));
#36225=CARTESIAN_POINT('Ctrl Pts',(13.0691860111115,-0.0819872800401352,
3.35412504823007));
#36226=CARTESIAN_POINT('Ctrl Pts',(13.0928001272613,0.234405401379786,3.39260352716186));
#36227=CARTESIAN_POINT('Ctrl Pts',(13.1164142434112,0.494621196584012,3.57664879910166));
#36228=CARTESIAN_POINT('Ctrl Pts',(13.1400283595611,0.636297578801308,3.86215313342763));
#36229=CARTESIAN_POINT('Ctrl Pts',(13.1636424757109,0.625480816776257,4.18069342892634));
#36230=CARTESIAN_POINT('Ctrl Pts',(13.1872565918608,0.464763222827219,4.45592928631477));
#36231=CARTESIAN_POINT('Ctrl Pts',(13.2077806665239,0.228267895462889,4.60018049807294));
#36232=CARTESIAN_POINT('Ctrl Pts',(13.220433369137,0.0625891701764018,4.62492503806923));
#36233=CARTESIAN_POINT('Ctrl Pts',(13.2252146997001,-9.32440196474427E-6,
4.62495874418382));
#36234=CARTESIAN_POINT('Ctrl Pts',(12.8247853002999,-1.55438223423052E-5,
4.62499607812274));
#36235=CARTESIAN_POINT('Ctrl Pts',(12.8267227422326,-0.0253767156259869,
4.62502109614712));
#36236=CARTESIAN_POINT('Ctrl Pts',(12.8365315562153,-0.153759343851268,
4.61735081595804));
#36237=CARTESIAN_POINT('Ctrl Pts',(12.854211742248,-0.376327535803878,4.5312757721487));
#36238=CARTESIAN_POINT('Ctrl Pts',(12.8778258583979,-0.583405888470749,
4.28898776831928));
#36239=CARTESIAN_POINT('Ctrl Pts',(12.9014399745477,-0.650666957548692,
3.97744183415536));
#36240=CARTESIAN_POINT('Ctrl Pts',(12.9250540906976,-0.561991161265395,
3.67130212143154));
#36241=CARTESIAN_POINT('Ctrl Pts',(12.9486682068475,-0.338630270727757,
3.44393714350224));
#36242=CARTESIAN_POINT('Ctrl Pts',(12.9722823229973,-0.0341142786054444,
3.34983650006563));
#36243=CARTESIAN_POINT('Ctrl Pts',(12.9958964391472,0.278577437919422,3.41155206540036));
#36244=CARTESIAN_POINT('Ctrl Pts',(13.0195105552971,0.524506132150044,3.61429327464512));
#36245=CARTESIAN_POINT('Ctrl Pts',(13.0431246714469,0.644733280558021,3.90947178565704));
#36246=CARTESIAN_POINT('Ctrl Pts',(13.0667387875968,0.61044561006836,4.22634601343335));
#36247=CARTESIAN_POINT('Ctrl Pts',(13.0903529037467,0.429860399609997,4.4889748434194));
#36248=CARTESIAN_POINT('Ctrl Pts',(13.1097017413144,0.197481915229314,4.60814700801091));
#36249=CARTESIAN_POINT('Ctrl Pts',(13.1211792068321,0.0472175377905832,
4.6249611028038));
#36250=CARTESIAN_POINT('Ctrl Pts',(13.1247853002999,3.84888821536311E-6,
4.62495078081483));
#36251=CARTESIAN_POINT('Origin',(11.8752146997001,0.,4.));
#36252=CARTESIAN_POINT('',(12.5247853002999,3.80998376854277E-6,4.62503871776264));
#36253=CARTESIAN_POINT('',(12.6252146997001,1.49489494596481E-5,4.6250110476872));
#36254=CARTESIAN_POINT('',(11.8752146997001,-1.68747709936658E-14,4.625));
#36255=CARTESIAN_POINT('',(12.5,0.310062960217711,4.54266560670548));
#36256=CARTESIAN_POINT('Ctrl Pts',(12.5,0.310062960217722,4.54266560670548));
#36257=CARTESIAN_POINT('Ctrl Pts',(12.50787137205,0.220600394030941,4.59378185169648));
#36258=CARTESIAN_POINT('Ctrl Pts',(12.5161331388166,0.113220056708515,4.6237347594226));
#36259=CARTESIAN_POINT('Ctrl Pts',(12.5243949055832,0.00511234815255113,
4.6250406321328));
#36260=CARTESIAN_POINT('Ctrl Pts',(12.5247853002999,3.80998376856706E-6,
4.62503871776264));
#36261=CARTESIAN_POINT('',(12.5,0.310062960217774,3.45733439329455));
#36262=CARTESIAN_POINT('Origin',(12.5,0.,4.));
#36263=CARTESIAN_POINT('Ctrl Pts',(12.5,0.310093463203755,3.45730861053195));
#36264=CARTESIAN_POINT('Ctrl Pts',(12.5008157411716,0.319367492808711,3.46259780682489));
#36265=CARTESIAN_POINT('Ctrl Pts',(12.5095028543931,0.416666480413896,3.52147574364868));
#36266=CARTESIAN_POINT('Ctrl Pts',(12.5260613396645,0.569511032758309,3.68451895614546));
#36267=CARTESIAN_POINT('Ctrl Pts',(12.5496754558144,0.651018771792273,3.99264764559437));
#36268=CARTESIAN_POINT('Ctrl Pts',(12.5732895719643,0.576495013506714,4.3025367374363));
#36269=CARTESIAN_POINT('Ctrl Pts',(12.5969036881141,0.363815091701307,4.53992168461618));
#36270=CARTESIAN_POINT('Ctrl Pts',(12.6142120640261,0.144017971622128,4.61907377583531));
#36271=CARTESIAN_POINT('Ctrl Pts',(12.6236490678881,0.0205077016108913,
4.62503160004571));
#36272=CARTESIAN_POINT('Ctrl Pts',(12.6252146997001,1.49489494596471E-5,
4.6250110476872));
#36273=CARTESIAN_POINT('Origin',(11.8752146997001,0.,4.));
#36274=CARTESIAN_POINT('Ctrl Pts',(12.6252146997001,1.49489494596471E-5,
4.6250110476872));
#36275=CARTESIAN_POINT('Ctrl Pts',(12.631520439938,-0.0825216819810338,
4.62492827098767));
#36276=CARTESIAN_POINT('Ctrl Pts',(12.6456975522259,-0.268159494659544,
4.5879440580038));
#36277=CARTESIAN_POINT('Ctrl Pts',(12.6677460365637,-0.506235857616531,
4.40939182910775));
#36278=CARTESIAN_POINT('Ctrl Pts',(12.6913601527136,-0.639894509617229,
4.12004729681268));
#36279=CARTESIAN_POINT('Ctrl Pts',(12.7149742688635,-0.620198095551099,
3.8019325752266));
#36280=CARTESIAN_POINT('Ctrl Pts',(12.7385883850133,-0.451866840211785,
3.53128609963859));
#36281=CARTESIAN_POINT('Ctrl Pts',(12.7622025011632,-0.17524257447904,3.37297016902465));
#36282=CARTESIAN_POINT('Ctrl Pts',(12.7858166173131,0.143379805101228,3.36492630429559));
#36283=CARTESIAN_POINT('Ctrl Pts',(12.809430733463,0.42764021116234,3.50908227080648));
#36284=CARTESIAN_POINT('Ctrl Pts',(12.8330448496128,0.609413666055986,3.77089008898231));
#36285=CARTESIAN_POINT('Ctrl Pts',(12.8566589657627,0.645136892431096,4.08760569204938));
#36286=CARTESIAN_POINT('Ctrl Pts',(12.8802730819125,0.526248572038732,4.38332598125533));
#36287=CARTESIAN_POINT('Ctrl Pts',(12.903124993225,0.289149347937084,4.5805996458561));
#36288=CARTESIAN_POINT('Ctrl Pts',(12.9181055324875,0.0930307802739178,
4.62497206165088));
#36289=CARTESIAN_POINT('Ctrl Pts',(12.9252146997001,-9.42225863212465E-6,
4.62504029123832));
#36290=CARTESIAN_POINT('Ctrl Pts',(12.5247853002999,3.80998376856706E-6,
4.62503871776264));
#36291=CARTESIAN_POINT('Ctrl Pts',(12.5322662776332,-0.0978890574527522,
4.62500203345524));
#36292=CARTESIAN_POINT('Ctrl Pts',(12.5476186270164,-0.298862923743373,
4.57698368148067));
#36293=CARTESIAN_POINT('Ctrl Pts',(12.5708423484496,-0.535054221536356,
4.37092866956447));
#36294=CARTESIAN_POINT('Ctrl Pts',(12.5944564645995,-0.647009713430093,
4.07251155115386));
#36295=CARTESIAN_POINT('Ctrl Pts',(12.6180705807493,-0.603894380709874,
3.75671714932517));
#36296=CARTESIAN_POINT('Ctrl Pts',(12.6416846968992,-0.416056506175611,
3.49922677321964));
#36297=CARTESIAN_POINT('Ctrl Pts',(12.6652988130491,-0.128505496873939,
3.36175035317655));
#36298=CARTESIAN_POINT('Ctrl Pts',(12.6889129291989,0.189841674427298,3.37723482234205));
#36299=CARTESIAN_POINT('Ctrl Pts',(12.7125270453488,0.462692468193658,3.54196933898577));
#36300=CARTESIAN_POINT('Ctrl Pts',(12.7361411614987,0.624655556881011,3.81647407445394));
#36301=CARTESIAN_POINT('Ctrl Pts',(12.7597552776485,0.636915702199809,4.13496208375113));
#36302=CARTESIAN_POINT('Ctrl Pts',(12.7833693937984,0.496534514683115,4.42110548633398));
#36303=CARTESIAN_POINT('Ctrl Pts',(12.8050460680155,0.258436396781676,4.5911312751119));
#36304=CARTESIAN_POINT('Ctrl Pts',(12.8188513701827,0.0776597756952025,
4.62491945378327));
#36305=CARTESIAN_POINT('Ctrl Pts',(12.8247853002999,-1.55438223423052E-5,
4.62499607812274));
#36306=CARTESIAN_POINT('Ctrl Pts',(12.5,-0.186196943290592,3.58169363627332));
#36307=CARTESIAN_POINT('Ctrl Pts',(12.50787137205,-0.117235947257613,3.55099764935784));
#36308=CARTESIAN_POINT('Ctrl Pts',(12.5236141161499,0.0360970477778841,
3.52440632583991));
#36309=CARTESIAN_POINT('Ctrl Pts',(12.5472282322997,0.257537368848111,3.59853698535937));
#36310=CARTESIAN_POINT('Ctrl Pts',(12.5708423484496,0.417223782598737,3.76887858727216));
#36311=CARTESIAN_POINT('Ctrl Pts',(12.5944564645995,0.476936352215019,3.99461366516243));
#36312=CARTESIAN_POINT('Ctrl Pts',(12.6180705807493,0.422340246895018,4.22163841384584));
#36313=CARTESIAN_POINT('Ctrl Pts',(12.6416846968992,0.266530936180377,4.39554662614981));
#36314=CARTESIAN_POINT('Ctrl Pts',(12.6652988130491,0.0468439715927196,
4.47465904879863));
#36315=CARTESIAN_POINT('Ctrl Pts',(12.6889129291989,-0.184068700558194,
4.44001626345752));
#36316=CARTESIAN_POINT('Ctrl Pts',(12.7125270453488,-0.37086838928987,4.29992045400434));
#36317=CARTESIAN_POINT('Ctrl Pts',(12.7361411614987,-0.468786717745582,
4.08794664964497));
#36318=CARTESIAN_POINT('Ctrl Pts',(12.7597552776485,-0.454357124800734,
3.85489580461101));
#36319=CARTESIAN_POINT('Ctrl Pts',(12.7833693937984,-0.331037647139153,
3.65662019659523));
#36320=CARTESIAN_POINT('Ctrl Pts',(12.8069835099483,-0.128382710063344,
3.54063794582746));
#36321=CARTESIAN_POINT('Ctrl Pts',(12.8305976260981,0.10504004521716,3.53474501052695));
#36322=CARTESIAN_POINT('Ctrl Pts',(12.854211742248,0.31328921869753,3.64035367159283));
#36323=CARTESIAN_POINT('Ctrl Pts',(12.8778258583979,0.446456451752615,3.83215407918844));
#36324=CARTESIAN_POINT('Ctrl Pts',(12.9014399745477,0.47262728739502,4.06417992999538));
#36325=CARTESIAN_POINT('Ctrl Pts',(12.9250540906976,0.385529703875575,4.28082461386765));
#36326=CARTESIAN_POINT('Ctrl Pts',(12.9486682068475,0.206037242841946,4.43016772408018));
#36327=CARTESIAN_POINT('Ctrl Pts',(12.9722823229973,-0.0228334776507366,
4.47641814468844));
#36328=CARTESIAN_POINT('Ctrl Pts',(12.9958964391472,-0.24623199631158,4.40849164040747));
#36329=CARTESIAN_POINT('Ctrl Pts',(13.0195105552971,-0.410619302934066,
4.24266727085754));
#36330=CARTESIAN_POINT('Ctrl Pts',(13.0431246714469,-0.476598835156983,
4.01868600055616));
#36331=CARTESIAN_POINT('Ctrl Pts',(13.0667387875968,-0.428358138764893,
3.79022650014263));
#36332=CARTESIAN_POINT('Ctrl Pts',(13.0903529037467,-0.277458432473742,
3.61204067927388));
#36333=CARTESIAN_POINT('Ctrl Pts',(13.1139670198965,-0.060063881357403,
3.52683201033335));
#36334=CARTESIAN_POINT('Ctrl Pts',(13.1375811360464,0.171725397050831,3.55502134399878));
#36335=CARTESIAN_POINT('Ctrl Pts',(13.1611952521963,0.362359488617447,3.68985291022187));
#36336=CARTESIAN_POINT('Ctrl Pts',(13.1848093683461,0.466151606229838,3.89901338554908));
#36337=CARTESIAN_POINT('Ctrl Pts',(13.208423484496,0.458227246370285,4.13237600603144));
#36338=CARTESIAN_POINT('Ctrl Pts',(13.2320376006459,0.34048553704322,4.3340137951542));
#36339=CARTESIAN_POINT('Ctrl Pts',(13.2556517167957,0.141144098528766,4.45560285308526));
#36340=CARTESIAN_POINT('Ctrl Pts',(13.2792658329456,-0.0920235057499227,
4.46800351566886));
#36341=CARTESIAN_POINT('Ctrl Pts',(13.3028799490955,-0.30313703626889,4.36824387779166));
#36342=CARTESIAN_POINT('Ctrl Pts',(13.3264940652453,-0.441601665806575,
4.18023203113149));
#36343=CARTESIAN_POINT('Ctrl Pts',(13.3501081813952,-0.47423338199515,3.94902632355453));
#36344=CARTESIAN_POINT('Ctrl Pts',(13.3737222975451,-0.393211766889608,
3.73003681238273));
#36345=CARTESIAN_POINT('Ctrl Pts',(13.3973364136949,-0.217954214568861,
3.57574585842847));
#36346=CARTESIAN_POINT('Ctrl Pts',(13.4209505298448,0.00953758252632317,
3.52313036287841));
#36347=CARTESIAN_POINT('Ctrl Pts',(13.4445646459947,0.234743631574736,3.58479999551538));
#36348=CARTESIAN_POINT('Ctrl Pts',(13.4681787621445,0.403691735186444,3.74597519957476));
#36349=CARTESIAN_POINT('Ctrl Pts',(13.4917928782944,0.475892304226004,3.96802921540861));
#36350=CARTESIAN_POINT('Ctrl Pts',(13.5154069944443,0.434041969710506,4.19774525232923));
#36351=CARTESIAN_POINT('Ctrl Pts',(13.5390211105941,0.288170455640921,4.38007026295756));
#36352=CARTESIAN_POINT('Ctrl Pts',(13.562635226744,0.0732368858249759,4.47130878927046));
#36353=CARTESIAN_POINT('Ctrl Pts',(13.5862493428939,-0.159248413505658,
4.44959488329479));
#36354=CARTESIAN_POINT('Ctrl Pts',(13.6098634590437,-0.353568721957589,
4.32013243375547));
#36355=CARTESIAN_POINT('Ctrl Pts',(13.6334775751936,-0.46315382488092,4.1139480179165));
#36356=CARTESIAN_POINT('Ctrl Pts',(13.6570916913435,-0.461740889501104,
3.88045516635315));
#36357=CARTESIAN_POINT('Ctrl Pts',(13.6807058074933,-0.349668535617837,
3.67561206636528));
#36358=CARTESIAN_POINT('Ctrl Pts',(13.7043199236432,-0.153795683012805,
3.5485107928471));
#36359=CARTESIAN_POINT('Ctrl Pts',(13.7279340397931,0.0789353756500159,
3.5296120507922));
#36360=CARTESIAN_POINT('Ctrl Pts',(13.7515481559429,0.292749022042461,3.62344505529457));
#36361=CARTESIAN_POINT('Ctrl Pts',(13.7751622720928,0.436403327377467,3.80752207362193));
#36362=CARTESIAN_POINT('Ctrl Pts',(13.7987763882427,0.475470537355291,4.03772776690975));
#36363=CARTESIAN_POINT('Ctrl Pts',(13.8223905043925,0.400587923144683,4.25889173822189));
#36364=CARTESIAN_POINT('Ctrl Pts',(13.8460046205424,0.229701624524423,4.41801050223621));
#36365=CARTESIAN_POINT('Ctrl Pts',(13.8696187366923,0.00376573255618155,
4.47695013947711));
#36366=CARTESIAN_POINT('Ctrl Pts',(13.8932328528421,-0.223072643433687,
4.42158535558109));
#36367=CARTESIAN_POINT('Ctrl Pts',(13.916846968992,-0.396450107540549,4.26518470642179));
#36368=CARTESIAN_POINT('Ctrl Pts',(13.9404610851419,-0.474815543552022,
4.04523069632808));
#36369=CARTESIAN_POINT('Ctrl Pts',(13.9640752012917,-0.439388129199652,
3.81443683499316));
#36370=CARTESIAN_POINT('Ctrl Pts',(13.9876893174416,-0.298658290955197,
3.62811447792009));
#36371=CARTESIAN_POINT('Ctrl Pts',(14.0113034335915,-0.0863529142219465,
3.53091707503438));
#36372=CARTESIAN_POINT('Ctrl Pts',(14.0349175497413,0.146647539536438,3.54613866056158));
#36373=CARTESIAN_POINT('Ctrl Pts',(14.0585316658912,0.344502889581789,3.6701312755675));
#36374=CARTESIAN_POINT('Ctrl Pts',(14.0821457820411,0.459795723937725,3.87317922671144));
#36375=CARTESIAN_POINT('Ctrl Pts',(14.1057598981909,0.464895312258427,4.10662065901627));
#36376=CARTESIAN_POINT('Ctrl Pts',(14.1293740143408,0.358579502702881,4.31450970816539));
#36377=CARTESIAN_POINT('Ctrl Pts',(14.1529881304907,0.166327619131383,4.44702431634421));
#36378=CARTESIAN_POINT('Ctrl Pts',(14.1766022466405,-0.0657858362277661,
4.47240643522367));
#36379=CARTESIAN_POINT('Ctrl Pts',(14.2002163627904,-0.282133257977474,
4.38457306332079));
#36380=CARTESIAN_POINT('Ctrl Pts',(14.2238304789403,-0.430865480427841,
4.20457407964992));
#36381=CARTESIAN_POINT('Ctrl Pts',(14.2474445950901,-0.476337791093329,
3.97554749368157));
#36382=CARTESIAN_POINT('Ctrl Pts',(14.27105871124,-0.407652434174819,3.75238112107461));
#36383=CARTESIAN_POINT('Ctrl Pts',(14.2946728273899,-0.241270333599833,
3.58855833656088));
#36384=CARTESIAN_POINT('Ctrl Pts',(14.3182869435397,-0.0170661180132474,
3.52334041087493));
#36385=CARTESIAN_POINT('Ctrl Pts',(14.3419010596896,0.211228111558234,3.57235727391142));
#36386=CARTESIAN_POINT('Ctrl Pts',(14.3655151758395,0.388900053764453,3.72386169322071));
#36387=CARTESIAN_POINT('Ctrl Pts',(14.3891292919893,0.473369390821204,3.94154458004181));
#36388=CARTESIAN_POINT('Ctrl Pts',(14.4127434081392,0.444392458083208,4.17323671518384));
#36389=CARTESIAN_POINT('Ctrl Pts',(14.4363575242891,0.308913779199362,4.3634114655727));
#36390=CARTESIAN_POINT('Ctrl Pts',(14.4599716404389,0.0994017626770733,
4.46649212840691));
#36391=CARTESIAN_POINT('Ctrl Pts',(14.4835857565888,-0.133932578240045,
4.45777470525894));
#36392=CARTESIAN_POINT('Ctrl Pts',(14.5071998727387,-0.335169044432007,
4.33934838727104));
#36393=CARTESIAN_POINT('Ctrl Pts',(14.5308139888885,-0.456079915900645,
4.13959486595487));
#36394=CARTESIAN_POINT('Ctrl Pts',(14.5544281050384,-0.467688060597361,
3.90638646324521));
#36395=CARTESIAN_POINT('Ctrl Pts',(14.5780422211883,-0.367211505836647,
3.69561319629505));
#36396=CARTESIAN_POINT('Ctrl Pts',(14.6016563373381,-0.178730157419731,
3.55778834579073));
#36397=CARTESIAN_POINT('Ctrl Pts',(14.625270453488,0.0525851174261518,3.52594259660587));
#36398=CARTESIAN_POINT('Ctrl Pts',(14.6488845696379,0.271298002813252,3.60770800421126));
#36399=CARTESIAN_POINT('Ctrl Pts',(14.6724986857877,0.424992433239313,3.78348891949988));
#36400=CARTESIAN_POINT('Ctrl Pts',(14.6961128019376,0.476834468501385,4.01115822240469));
#36401=CARTESIAN_POINT('Ctrl Pts',(14.7197269180875,0.414399804028447,4.23615337970372));
#36402=CARTESIAN_POINT('Ctrl Pts',(14.7433410342373,0.252651341641402,4.40455273546398));
#36403=CARTESIAN_POINT('Ctrl Pts',(14.7669551503872,0.0303532266559796,
4.47599821226155));
#36404=CARTESIAN_POINT('Ctrl Pts',(14.7905692665371,-0.199219250862459,
4.43336740322118));
#36405=CARTESIAN_POINT('Ctrl Pts',(14.8141833826869,-0.381047447081096,
4.28687708064914));
#36406=CARTESIAN_POINT('Ctrl Pts',(14.8377974988368,-0.471554972144783,
4.07163466550741));
#36407=CARTESIAN_POINT('Ctrl Pts',(14.8614116149867,-0.449051060899263,
3.83922451083896));
#36408=CARTESIAN_POINT('Ctrl Pts',(14.8850257311365,-0.318928946727196,
3.64534530693059));
#36409=CARTESIAN_POINT('Ctrl Pts',(14.9086398472864,-0.112373269271187,
3.53646160000302));
#36410=CARTESIAN_POINT('Ctrl Pts',(14.9322539634362,0.121113399391719,3.5386680312482));
#36411=CARTESIAN_POINT('Ctrl Pts',(14.9558680795861,0.325574495333277,3.65143602219853));
#36412=CARTESIAN_POINT('Ctrl Pts',(14.979482195736,0.452009190454857,3.84773949289016));
#36413=CARTESIAN_POINT('Ctrl Pts',(15.0030963118858,0.470117180575255,4.08053390545391));
#36414=CARTESIAN_POINT('Ctrl Pts',(15.0267104280357,0.375557372208547,4.29402641177155));
#36415=CARTESIAN_POINT('Ctrl Pts',(15.0503245441856,0.190994688421392,4.43705643304037));
#36416=CARTESIAN_POINT('Ctrl Pts',(15.0739386603355,-0.0393454023191647,
4.47533644032795));
#36417=CARTESIAN_POINT('Ctrl Pts',(15.0975527764853,-0.260245916509526,
4.39971253597763));
#36418=CARTESIAN_POINT('Ctrl Pts',(15.1211668926352,-0.418792603204267,
4.22826540530875));
#36419=CARTESIAN_POINT('Ctrl Pts',(15.1369096367351,-0.457530945318996,
4.07754232577813));
#36420=CARTESIAN_POINT('Ctrl Pts',(15.1447810087851,-0.457870370902723,
4.00205890126089));
#36421=CARTESIAN_POINT('Ctrl Pts',(12.4850729970717,-0.208850989443975,
3.53079950502365));
#36422=CARTESIAN_POINT('Ctrl Pts',(12.4929443691216,-0.131499707516366,
3.49636882573344));
#36423=CARTESIAN_POINT('Ctrl Pts',(12.5086871132215,0.0404888716816997,
3.46654221242176));
#36424=CARTESIAN_POINT('Ctrl Pts',(12.5323012293714,0.288871199237585,3.54969213591223));
#36425=CARTESIAN_POINT('Ctrl Pts',(12.5559153455212,0.467986199318594,3.74075871022993));
#36426=CARTESIAN_POINT('Ctrl Pts',(12.5795294616711,0.534963825407437,3.99395832530641));
#36427=CARTESIAN_POINT('Ctrl Pts',(12.603143577821,0.473725169098917,4.24860452170932));
#36428=CARTESIAN_POINT('Ctrl Pts',(12.6267576939708,0.298958988020687,4.4436716456386));
#36429=CARTESIAN_POINT('Ctrl Pts',(12.6503718101207,0.0525433427838623,
4.53240944903922));
#36430=CARTESIAN_POINT('Ctrl Pts',(12.6739859262706,-0.206463809544117,
4.49355177571912));
#36431=CARTESIAN_POINT('Ctrl Pts',(12.6976000424205,-0.41599087873209,4.33641091237214));
#36432=CARTESIAN_POINT('Ctrl Pts',(12.7212141585703,-0.525822648369464,
4.09864686536754));
#36433=CARTESIAN_POINT('Ctrl Pts',(12.7448282747202,-0.509637448384189,
3.8372413948162));
#36434=CARTESIAN_POINT('Ctrl Pts',(12.76844239087,-0.37131404483003,3.61484216427635));
#36435=CARTESIAN_POINT('Ctrl Pts',(12.7920565070199,-0.144002664868576,
3.48474868689319));
#36436=CARTESIAN_POINT('Ctrl Pts',(12.8156706231698,0.117819965178516,3.47813877511649));
#36437=CARTESIAN_POINT('Ctrl Pts',(12.8392847393197,0.351406216185799,3.59659653799738));
#36438=CARTESIAN_POINT('Ctrl Pts',(12.8628988554695,0.500775523187073,3.81173274911973));
#36439=CARTESIAN_POINT('Ctrl Pts',(12.8865129716194,0.530130489073712,4.07198851734671));
#36440=CARTESIAN_POINT('Ctrl Pts',(12.9101270877692,0.432435993263294,4.31499173633021));
#36441=CARTESIAN_POINT('Ctrl Pts',(12.9337412039191,0.231105201134755,4.48250499290311));
#36442=CARTESIAN_POINT('Ctrl Pts',(12.957355320069,-0.0256115611541523,
4.53438256906268));
#36443=CARTESIAN_POINT('Ctrl Pts',(12.9809694362189,-0.276190334565159,
4.45819164252092));
#36444=CARTESIAN_POINT('Ctrl Pts',(13.0045835523687,-0.460578171623014,
4.27219189922559));
#36445=CARTESIAN_POINT('Ctrl Pts',(13.0281976685186,-0.534585243620437,
4.0209594724593));
#36446=CARTESIAN_POINT('Ctrl Pts',(13.0518117846684,-0.480475240551103,
3.76470396221295));
#36447=CARTESIAN_POINT('Ctrl Pts',(13.0754259008183,-0.311216001335094,
3.5648387853972));
#36448=CARTESIAN_POINT('Ctrl Pts',(13.0990400169682,-0.0673716809183137,
3.46926302296559));
#36449=CARTESIAN_POINT('Ctrl Pts',(13.122654133118,0.19261873182715,3.50088207171981));
#36450=CARTESIAN_POINT('Ctrl Pts',(13.1462682492679,0.406446724606302,3.65211820651514));
#36451=CARTESIAN_POINT('Ctrl Pts',(13.1698823654178,0.522866930420328,3.88672663484193));
#36452=CARTESIAN_POINT('Ctrl Pts',(13.1934964815676,0.513978436505609,4.14848181366307));
#36453=CARTESIAN_POINT('Ctrl Pts',(13.2171105977175,0.381911432304553,4.37465229220773));
#36454=CARTESIAN_POINT('Ctrl Pts',(13.2407247138674,0.158316694737061,4.51103474084347));
#36455=CARTESIAN_POINT('Ctrl Pts',(13.2643388300172,-0.103219740820234,
4.52494415635039));
#36456=CARTESIAN_POINT('Ctrl Pts',(13.2879529461671,-0.340018846942428,
4.41304705047411));
#36457=CARTESIAN_POINT('Ctrl Pts',(13.311567062317,-0.495330069408668,4.20216034359148));
#36458=CARTESIAN_POINT('Ctrl Pts',(13.3351811784669,-0.531931992580964,
3.94282450306062));
#36459=CARTESIAN_POINT('Ctrl Pts',(13.3587952946167,-0.44105271077271,3.69719116838925));
#36460=CARTESIAN_POINT('Ctrl Pts',(13.3824094107666,-0.244472076510672,
3.5241280781681));
#36461=CARTESIAN_POINT('Ctrl Pts',(13.4060235269164,0.0106979927399635,
3.46511100671938));
#36462=CARTESIAN_POINT('Ctrl Pts',(13.4296376430663,0.263304213558122,3.53428380605355));
#36463=CARTESIAN_POINT('Ctrl Pts',(13.4532517592162,0.452807746647384,3.71506873327496));
#36464=CARTESIAN_POINT('Ctrl Pts',(13.476865875366,0.533792751104717,3.96413942206993));
#36465=CARTESIAN_POINT('Ctrl Pts',(13.5004799915159,0.486850606847911,4.22180434800346));
#36466=CARTESIAN_POINT('Ctrl Pts',(13.5240941076658,0.323231325528255,4.42631231788287));
#36467=CARTESIAN_POINT('Ctrl Pts',(13.5477082238157,0.0821474069231642,
4.52865157307741));
#36468=CARTESIAN_POINT('Ctrl Pts',(13.5713223399655,-0.178623709606947,
4.50429579866153));
#36469=CARTESIAN_POINT('Ctrl Pts',(13.5949364561154,-0.396586410669692,
4.35908202552279));
#36470=CARTESIAN_POINT('Ctrl Pts',(13.6185505722652,-0.519504417643299,
4.12781174527607));
#36471=CARTESIAN_POINT('Ctrl Pts',(13.6421646884151,-0.517919574482721,
3.86591049053316));
#36472=CARTESIAN_POINT('Ctrl Pts',(13.665778804565,-0.392211699884016,3.6361447201764));
#36473=CARTESIAN_POINT('Ctrl Pts',(13.6893929207148,-0.172507561089802,
3.49357940054904));
#36474=CARTESIAN_POINT('Ctrl Pts',(13.7130070368647,0.0885392156030666,
3.47238130294519));
#36475=CARTESIAN_POINT('Ctrl Pts',(13.7366211530146,0.328366952925232,3.57763069902274));
#36476=CARTESIAN_POINT('Ctrl Pts',(13.7602352691644,0.489499264105438,3.78410383833506));
#36477=CARTESIAN_POINT('Ctrl Pts',(13.7838493853143,0.533319669072828,4.04231799571659));
#36478=CARTESIAN_POINT('Ctrl Pts',(13.8074635014642,0.449326302728307,4.29039035083475));
#36479=CARTESIAN_POINT('Ctrl Pts',(13.831077617614,0.257648760022572,4.46886863686992));
#36480=CARTESIAN_POINT('Ctrl Pts',(13.8546917337639,0.00422389839726028,
4.53497929012603));
#36481=CARTESIAN_POINT('Ctrl Pts',(13.8783058499138,-0.25021324988294,4.47287843233165));
#36482=CARTESIAN_POINT('Ctrl Pts',(13.9019199660636,-0.444685051009628,
4.29744896636227));
#36483=CARTESIAN_POINT('Ctrl Pts',(13.9255340822135,-0.532584984058807,
4.05073378496132));
#36484=CARTESIAN_POINT('Ctrl Pts',(13.9491481983634,-0.492847218174075,
3.79185989881933));
#36485=CARTESIAN_POINT('Ctrl Pts',(13.9727623145132,-0.334995185577738,
3.58286823685896));
#36486=CARTESIAN_POINT('Ctrl Pts',(13.9963764306631,-0.0968592247428986,
3.47384510573062));
#36487=CARTESIAN_POINT('Ctrl Pts',(14.019990546813,0.164489723571401,3.49091865775613));
#36488=CARTESIAN_POINT('Ctrl Pts',(14.0436046629628,0.386417564563212,3.62999709733779));
#36489=CARTESIAN_POINT('Ctrl Pts',(14.0672187791127,0.515737746224078,3.85774930825782));
#36490=CARTESIAN_POINT('Ctrl Pts',(14.0908328952626,0.521457786777448,4.11959288770904));
#36491=CARTESIAN_POINT('Ctrl Pts',(14.1144470114124,0.402206838685568,4.35277519909424));
#36492=CARTESIAN_POINT('Ctrl Pts',(14.1380611275623,0.186564221804844,4.50141247822903));
#36493=CARTESIAN_POINT('Ctrl Pts',(14.1616752437122,-0.0737898095680628,
4.52988276645436));
#36494=CARTESIAN_POINT('Ctrl Pts',(14.185289359862,-0.316459599402161,4.43136296100575));
#36495=CARTESIAN_POINT('Ctrl Pts',(14.2089034760119,-0.483287643257218,
4.22946401908862));
#36496=CARTESIAN_POINT('Ctrl Pts',(14.2325175921618,-0.53429243907693,3.97257242762026));
#36497=CARTESIAN_POINT('Ctrl Pts',(14.2561317083116,-0.457250332481466,
3.72225404480531));
#36498=CARTESIAN_POINT('Ctrl Pts',(14.2797458244615,-0.270625000632592,
3.53849941363631));
#36499=CARTESIAN_POINT('Ctrl Pts',(14.3033599406114,-0.0191425034699505,
3.46534661065105));
#36500=CARTESIAN_POINT('Ctrl Pts',(14.3269740567612,0.236927627906706,3.52032721432634));
#36501=CARTESIAN_POINT('Ctrl Pts',(14.3505881729111,0.436216403922163,3.69026474025285));
#36502=CARTESIAN_POINT('Ctrl Pts',(14.374202289061,0.530962882087739,3.93443247734966));
#36503=CARTESIAN_POINT('Ctrl Pts',(14.3978164052108,0.498460409348769,4.19431392768733));
#36504=CARTESIAN_POINT('Ctrl Pts',(14.4214305213607,0.346498429557861,4.40762669256976));
#36505=CARTESIAN_POINT('Ctrl Pts',(14.4450446375106,0.111495689030631,4.52324888295055));
#36506=CARTESIAN_POINT('Ctrl Pts',(14.4686587536604,-0.150227769531968,
4.51347083601981));
#36507=CARTESIAN_POINT('Ctrl Pts',(14.4922728698103,-0.375948097339969,
4.38063592879268));
#36508=CARTESIAN_POINT('Ctrl Pts',(14.5158869859602,-0.51156984651846,4.15657897149511));
#36509=CARTESIAN_POINT('Ctrl Pts',(14.53950110211,-0.52459032076832,3.89499677367918));
#36510=CARTESIAN_POINT('Ctrl Pts',(14.5631152182599,-0.411889072794842,
3.65857933001481));
#36511=CARTESIAN_POINT('Ctrl Pts',(14.5867293344098,-0.200475741228102,
3.50398572665543));
#36512=CARTESIAN_POINT('Ctrl Pts',(14.6103434505596,0.0589829973059192,
3.46826539682992));
#36513=CARTESIAN_POINT('Ctrl Pts',(14.6339575667095,0.304306049929579,3.5599789662306));
#36514=CARTESIAN_POINT('Ctrl Pts',(14.6575716828594,0.476700039321847,3.75714663952638));
#36515=CARTESIAN_POINT('Ctrl Pts',(14.6811857990092,0.53484954579562,4.0125158112076));
#36516=CARTESIAN_POINT('Ctrl Pts',(14.7047999151591,0.464818635404008,4.26488548168423));
#36517=CARTESIAN_POINT('Ctrl Pts',(14.728414031309,0.283390703164248,4.45377350235044));
#36518=CARTESIAN_POINT('Ctrl Pts',(14.7520281474588,0.0340462163765225,
4.5339115446661));
#36519=CARTESIAN_POINT('Ctrl Pts',(14.7756422636087,-0.223457683695575,
4.48609396779546));
#36520=CARTESIAN_POINT('Ctrl Pts',(14.7992563797586,-0.427408393186059,
4.32178058932398));
#36521=CARTESIAN_POINT('Ctrl Pts',(14.8228704959084,-0.528927708313459,
4.08035024907128));
#36522=CARTESIAN_POINT('Ctrl Pts',(14.8464846120583,-0.503685810960444,
3.81966341983811));
#36523=CARTESIAN_POINT('Ctrl Pts',(14.8700987282082,-0.357732113691821,
3.6021954912391));
#36524=CARTESIAN_POINT('Ctrl Pts',(14.893712844358,-0.126045401495737,3.48006421709321));
#36525=CARTESIAN_POINT('Ctrl Pts',(14.9173269605079,0.13584891809103,3.48253909847714));
#36526=CARTESIAN_POINT('Ctrl Pts',(14.9409410766578,0.365186207068703,3.60902724630258));
#36527=CARTESIAN_POINT('Ctrl Pts',(14.9645551928076,0.507003847624586,3.82921439524653));
#36528=CARTESIAN_POINT('Ctrl Pts',(14.9881693089575,0.52731498478211,4.0903322339271));
#36529=CARTESIAN_POINT('Ctrl Pts',(15.0117834251074,0.421250356706029,4.32979975898591));
#36530=CARTESIAN_POINT('Ctrl Pts',(15.0353975412572,0.214232462415332,4.49023183125449));
#36531=CARTESIAN_POINT('Ctrl Pts',(15.0590116574071,-0.0441324441701724,
4.53316925684615));
#36532=CARTESIAN_POINT('Ctrl Pts',(15.082625773557,-0.291909288096862,4.4483444097243));
#36533=CARTESIAN_POINT('Ctrl Pts',(15.1062398897068,-0.469745893811612,
4.25603780014884));
#36534=CARTESIAN_POINT('Ctrl Pts',(15.1219826338067,-0.513197418509596,
4.08697667736293));
#36535=CARTESIAN_POINT('Ctrl Pts',(15.1298540058567,-0.513578141027115,
4.0023094018511));
#36536=CARTESIAN_POINT('Ctrl Pts',(12.4701459941433,-0.231505035597357,
3.47990537377399));
#36537=CARTESIAN_POINT('Ctrl Pts',(12.4780173661933,-0.145763467775118,
3.44174000210903));
#36538=CARTESIAN_POINT('Ctrl Pts',(12.4937601102932,0.0448806955855158,
3.40867809900361));
#36539=CARTESIAN_POINT('Ctrl Pts',(12.517374226443,0.320205029627059,3.5008472864651));
#36540=CARTESIAN_POINT('Ctrl Pts',(12.5409883425929,0.518748616038451,3.71263883318769));
#36541=CARTESIAN_POINT('Ctrl Pts',(12.5646024587428,0.592991298599855,3.99330298545039));
#36542=CARTESIAN_POINT('Ctrl Pts',(12.5882165748926,0.525110091302815,4.27557062957281));
#36543=CARTESIAN_POINT('Ctrl Pts',(12.6118306910425,0.331387039860997,4.49179666512739));
#36544=CARTESIAN_POINT('Ctrl Pts',(12.6354448071924,0.0582427139750047,
4.5901598492798));
#36545=CARTESIAN_POINT('Ctrl Pts',(12.6590589233422,-0.22885891853004,4.54708728798072));
#36546=CARTESIAN_POINT('Ctrl Pts',(12.6826730394921,-0.461113368174311,
4.37290137073994));
#36547=CARTESIAN_POINT('Ctrl Pts',(12.706287155642,-0.582858578993347,4.10934708109011));
#36548=CARTESIAN_POINT('Ctrl Pts',(12.7299012717918,-0.564917771967644,
3.8195869850214));
#36549=CARTESIAN_POINT('Ctrl Pts',(12.7535153879417,-0.411590442520908,
3.57306413195747));
#36550=CARTESIAN_POINT('Ctrl Pts',(12.7771295040916,-0.159622619673808,
3.42885942795892));
#36551=CARTESIAN_POINT('Ctrl Pts',(12.8007436202414,0.130599885139872,3.42153253970604));
#36552=CARTESIAN_POINT('Ctrl Pts',(12.8243577363913,0.38952321367407,3.55283940440193));
#36553=CARTESIAN_POINT('Ctrl Pts',(12.8479718525412,0.555094594621529,3.79131141905102));
#36554=CARTESIAN_POINT('Ctrl Pts',(12.871585968691,0.587633690752404,4.07979710469805));
#36555=CARTESIAN_POINT('Ctrl Pts',(12.8952000848409,0.479342282651013,4.34915885879276));
#36556=CARTESIAN_POINT('Ctrl Pts',(12.9188142009908,0.256173159427565,4.53484226172604));
#36557=CARTESIAN_POINT('Ctrl Pts',(12.9424283171406,-0.0283896446575681,
4.59234699343691));
#36558=CARTESIAN_POINT('Ctrl Pts',(12.9660424332905,-0.306148672818738,
4.50789164463438));
#36559=CARTESIAN_POINT('Ctrl Pts',(12.9896565494404,-0.510537040311962,
4.30171652759364));
#36560=CARTESIAN_POINT('Ctrl Pts',(13.0132706655902,-0.59257165208389,4.02323294436244));
#36561=CARTESIAN_POINT('Ctrl Pts',(13.0368847817401,-0.532592342337314,
3.73918142428326));
#36562=CARTESIAN_POINT('Ctrl Pts',(13.06049889789,-0.344973570196446,3.51763689152052));
#36563=CARTESIAN_POINT('Ctrl Pts',(13.0841130140398,-0.0746794804792245,
3.41169403559782));
#36564=CARTESIAN_POINT('Ctrl Pts',(13.1077271301897,0.213512066603468,3.44674279944083));
#36565=CARTESIAN_POINT('Ctrl Pts',(13.1313412463396,0.450533960595157,3.6143835028084));
#36566=CARTESIAN_POINT('Ctrl Pts',(13.1549553624894,0.579582254610818,3.87443988413478));
#36567=CARTESIAN_POINT('Ctrl Pts',(13.1785694786393,0.569729626640933,4.1645876212947));
#36568=CARTESIAN_POINT('Ctrl Pts',(13.2021835947892,0.423337327565886,4.41529078926125));
#36569=CARTESIAN_POINT('Ctrl Pts',(13.225797710939,0.175489290945357,4.56646662860168));
#36570=CARTESIAN_POINT('Ctrl Pts',(13.2494118270889,-0.114415975890545,
4.58188479703192));
#36571=CARTESIAN_POINT('Ctrl Pts',(13.2730259432388,-0.376900657615966,
4.45785022315656));
#36572=CARTESIAN_POINT('Ctrl Pts',(13.2966400593886,-0.54905847301076,4.22408865605146));
#36573=CARTESIAN_POINT('Ctrl Pts',(13.3202541755385,-0.589630603166779,
3.93662268256671));
#36574=CARTESIAN_POINT('Ctrl Pts',(13.3438682916884,-0.488893654655812,
3.66434552439578));
#36575=CARTESIAN_POINT('Ctrl Pts',(13.3674824078382,-0.270989938452484,
3.47251029790774));
#36576=CARTESIAN_POINT('Ctrl Pts',(13.3910965239881,0.0118584029536041,
3.40709165056035));
#36577=CARTESIAN_POINT('Ctrl Pts',(13.414710640138,0.291864795541507,3.48376761659174));
#36578=CARTESIAN_POINT('Ctrl Pts',(13.4383247562878,0.501923758108325,3.68416226697515));
#36579=CARTESIAN_POINT('Ctrl Pts',(13.4619388724377,0.591693197983429,3.96024962873126));
#36580=CARTESIAN_POINT('Ctrl Pts',(13.4855529885876,0.539659243985316,4.2458634436777));
#36581=CARTESIAN_POINT('Ctrl Pts',(13.5091671047374,0.358292195415589,4.47255437280819));
#36582=CARTESIAN_POINT('Ctrl Pts',(13.5327812208873,0.0910579280213527,
4.58599435688436));
#36583=CARTESIAN_POINT('Ctrl Pts',(13.5563953370372,-0.197999005708236,
4.55899671402827));
#36584=CARTESIAN_POINT('Ctrl Pts',(13.580009453187,-0.439604099381795,4.39803161729011));
#36585=CARTESIAN_POINT('Ctrl Pts',(13.6036235693369,-0.575855010405679,
4.14167547263565));
#36586=CARTESIAN_POINT('Ctrl Pts',(13.6272376854868,-0.574098259464336,
3.85136581471317));
#36587=CARTESIAN_POINT('Ctrl Pts',(13.6508518016366,-0.434754864150196,
3.59667737398752));
#36588=CARTESIAN_POINT('Ctrl Pts',(13.6744659177865,-0.191219439166798,
3.43864800825098));
#36589=CARTESIAN_POINT('Ctrl Pts',(13.6980800339364,0.0981430555561168,
3.41515055509818));
#36590=CARTESIAN_POINT('Ctrl Pts',(13.7216941500862,0.363984883808003,3.53181634275091));
#36591=CARTESIAN_POINT('Ctrl Pts',(13.7453082662361,0.54259520083341,3.76068560304818));
#36592=CARTESIAN_POINT('Ctrl Pts',(13.768922382386,0.591168800790367,4.04690822452342));
#36593=CARTESIAN_POINT('Ctrl Pts',(13.7925364985358,0.498064682311931,4.32188896344761));
#36594=CARTESIAN_POINT('Ctrl Pts',(13.8161506146857,0.28559589552072,4.51972677150362));
#36595=CARTESIAN_POINT('Ctrl Pts',(13.8397647308356,0.00468206423833927,
4.59300844077494));
#36596=CARTESIAN_POINT('Ctrl Pts',(13.8633788469854,-0.277353856332193,
4.52417150908221));
#36597=CARTESIAN_POINT('Ctrl Pts',(13.8869929631353,-0.492919994478707,
4.32971322630275));
#36598=CARTESIAN_POINT('Ctrl Pts',(13.9106070792852,-0.590354424565592,
4.05623687359455));
#36599=CARTESIAN_POINT('Ctrl Pts',(13.934221195435,-0.546306307148498,3.76928296264551));
#36600=CARTESIAN_POINT('Ctrl Pts',(13.9578353115849,-0.371332080200278,
3.53762199579782));
#36601=CARTESIAN_POINT('Ctrl Pts',(13.9814494277348,-0.107365535263851,
3.41677313642685));
#36602=CARTESIAN_POINT('Ctrl Pts',(14.0050635438846,0.182331907606365,3.43569865495067));
#36603=CARTESIAN_POINT('Ctrl Pts',(14.0286776600345,0.428332239544634,3.58986291910809));
#36604=CARTESIAN_POINT('Ctrl Pts',(14.0522917761844,0.571679768510432,3.8423193898042));
#36605=CARTESIAN_POINT('Ctrl Pts',(14.0759058923342,0.578020261296468,4.1325651164018));
#36606=CARTESIAN_POINT('Ctrl Pts',(14.0995200084841,0.445834174668256,4.39104069002309));
#36607=CARTESIAN_POINT('Ctrl Pts',(14.123134124634,0.206800824478305,4.55580064011384));
#36608=CARTESIAN_POINT('Ctrl Pts',(14.1467482407838,-0.0817937829083601,
4.58735909768505));
#36609=CARTESIAN_POINT('Ctrl Pts',(14.1703623569337,-0.350785940826847,
4.4781528586907));
#36610=CARTESIAN_POINT('Ctrl Pts',(14.1939764730836,-0.535709806086595,
4.25435395852733));
#36611=CARTESIAN_POINT('Ctrl Pts',(14.2175905892334,-0.59224708706053,3.96959736155895));
#36612=CARTESIAN_POINT('Ctrl Pts',(14.2412047053833,-0.506848230788112,
3.69212696853602));
#36613=CARTESIAN_POINT('Ctrl Pts',(14.2648188215332,-0.29997966766535,3.48844049071174));
#36614=CARTESIAN_POINT('Ctrl Pts',(14.288432937683,-0.0212188889266537,
3.40735281042717));
#36615=CARTESIAN_POINT('Ctrl Pts',(14.3120470538329,0.262627144255178,3.46829715474127));
#36616=CARTESIAN_POINT('Ctrl Pts',(14.3356611699828,0.483532754079872,3.65666778728498));
#36617=CARTESIAN_POINT('Ctrl Pts',(14.3592752861326,0.588556373354274,3.9273203746575));
#36618=CARTESIAN_POINT('Ctrl Pts',(14.3828894022825,0.55252836061433,4.21539114019081));
#36619=CARTESIAN_POINT('Ctrl Pts',(14.4065035184324,0.384083079916361,4.45184191956682));
#36620=CARTESIAN_POINT('Ctrl Pts',(14.4301176345822,0.123589615384189,4.58000563749418));
#36621=CARTESIAN_POINT('Ctrl Pts',(14.4537317507321,-0.166522960823891,
4.56916696678068));
#36622=CARTESIAN_POINT('Ctrl Pts',(14.477345866882,-0.416727150247931,4.42192347031433));
#36623=CARTESIAN_POINT('Ctrl Pts',(14.5009599830318,-0.567059777136274,
4.17356307703535));
#36624=CARTESIAN_POINT('Ctrl Pts',(14.5245740991817,-0.58149258093928,3.88360708411314));
#36625=CARTESIAN_POINT('Ctrl Pts',(14.5481882153316,-0.456566639753037,
3.62154546373458));
#36626=CARTESIAN_POINT('Ctrl Pts',(14.5718023314814,-0.222221325036472,
3.45018310752014));
#36627=CARTESIAN_POINT('Ctrl Pts',(14.5954164476313,0.0653808771856868,
3.41058819705396));
#36628=CARTESIAN_POINT('Ctrl Pts',(14.6190305637812,0.337314097045906,3.51224992824993));
#36629=CARTESIAN_POINT('Ctrl Pts',(14.642644679931,0.528407645404381,3.73080435955289));
#36630=CARTESIAN_POINT('Ctrl Pts',(14.6662587960809,0.592864623089856,4.0138734000105));
#36631=CARTESIAN_POINT('Ctrl Pts',(14.6898729122308,0.515237466779568,4.29361758366474));
#36632=CARTESIAN_POINT('Ctrl Pts',(14.7134870283806,0.314130064687094,4.5029942692369));
#36633=CARTESIAN_POINT('Ctrl Pts',(14.7371011445305,0.0377392060970651,
4.59182487707066));
#36634=CARTESIAN_POINT('Ctrl Pts',(14.7607152606804,-0.24769611652869,4.53882053236973));
#36635=CARTESIAN_POINT('Ctrl Pts',(14.7843293768302,-0.47376933929102,4.35668409799883));
#36636=CARTESIAN_POINT('Ctrl Pts',(14.8079434929801,-0.586300444482135,
4.08906583263515));
#36637=CARTESIAN_POINT('Ctrl Pts',(14.83155760913,-0.558320561021625,3.80010232883727));
#36638=CARTESIAN_POINT('Ctrl Pts',(14.8551717252798,-0.396535280656446,
3.55904567554761));
#36639=CARTESIAN_POINT('Ctrl Pts',(14.8787858414297,-0.139717533720287,
3.42366683418339));
#36640=CARTESIAN_POINT('Ctrl Pts',(14.9023999575795,0.150584436790342,3.42641016570609));
#36641=CARTESIAN_POINT('Ctrl Pts',(14.9260140737294,0.404797918804129,3.56661847040663));
#36642=CARTESIAN_POINT('Ctrl Pts',(14.9496281898793,0.561998504794314,3.8106892976029));
#36643=CARTESIAN_POINT('Ctrl Pts',(14.9732423060292,0.584512788988964,4.10013056240029));
#36644=CARTESIAN_POINT('Ctrl Pts',(14.996856422179,0.466943341203511,4.36557310620026));
#36645=CARTESIAN_POINT('Ctrl Pts',(15.0204705383289,0.237470236409271,4.54340722946861));
#36646=CARTESIAN_POINT('Ctrl Pts',(15.0440846544788,-0.0489194860211801,
4.59100207336435));
#36647=CARTESIAN_POINT('Ctrl Pts',(15.0676987706286,-0.323572659684198,
4.49697628347096));
#36648=CARTESIAN_POINT('Ctrl Pts',(15.0913128867785,-0.520699184418956,
4.28381019498893));
#36649=CARTESIAN_POINT('Ctrl Pts',(15.1070556308784,-0.568863891700195,
4.09641102894772));
#36650=CARTESIAN_POINT('Ctrl Pts',(15.1149270029284,-0.569285911151507,
4.00255990244131));
#36651=CARTESIAN_POINT('Ctrl Pts',(12.455218991215,-0.25415908175074,3.42901124252432));
#36652=CARTESIAN_POINT('Ctrl Pts',(12.4630903632649,-0.16002722803387,3.38711117848463));
#36653=CARTESIAN_POINT('Ctrl Pts',(12.4788331073648,0.0492725194893315,
3.35081398558546));
#36654=CARTESIAN_POINT('Ctrl Pts',(12.5024472235147,0.351538860016532,3.45200243701797));
#36655=CARTESIAN_POINT('Ctrl Pts',(12.5260613396645,0.569511032758309,3.68451895614546));
#36656=CARTESIAN_POINT('Ctrl Pts',(12.5496754558144,0.651018771792273,3.99264764559437));
#36657=CARTESIAN_POINT('Ctrl Pts',(12.5732895719643,0.576495013506714,4.3025367374363));
#36658=CARTESIAN_POINT('Ctrl Pts',(12.5969036881141,0.363815091701307,4.53992168461618));
#36659=CARTESIAN_POINT('Ctrl Pts',(12.620517804264,0.0639420851661475,4.64791024952038));
#36660=CARTESIAN_POINT('Ctrl Pts',(12.6441319204139,-0.251254027515963,
4.60062280024232));
#36661=CARTESIAN_POINT('Ctrl Pts',(12.6677460365637,-0.506235857616531,
4.40939182910775));
#36662=CARTESIAN_POINT('Ctrl Pts',(12.6913601527136,-0.639894509617229,
4.12004729681268));
#36663=CARTESIAN_POINT('Ctrl Pts',(12.7149742688635,-0.620198095551099,
3.8019325752266));
#36664=CARTESIAN_POINT('Ctrl Pts',(12.7385883850133,-0.451866840211785,
3.53128609963859));
#36665=CARTESIAN_POINT('Ctrl Pts',(12.7622025011632,-0.17524257447904,3.37297016902465));
#36666=CARTESIAN_POINT('Ctrl Pts',(12.7858166173131,0.143379805101228,3.36492630429559));
#36667=CARTESIAN_POINT('Ctrl Pts',(12.809430733463,0.42764021116234,3.50908227080648));
#36668=CARTESIAN_POINT('Ctrl Pts',(12.8330448496128,0.609413666055986,3.77089008898231));
#36669=CARTESIAN_POINT('Ctrl Pts',(12.8566589657627,0.645136892431096,4.08760569204938));
#36670=CARTESIAN_POINT('Ctrl Pts',(12.8802730819125,0.526248572038732,4.38332598125533));
#36671=CARTESIAN_POINT('Ctrl Pts',(12.9038871980624,0.281241117720374,4.58717953054897));
#36672=CARTESIAN_POINT('Ctrl Pts',(12.9275013142123,-0.0311677281609838,
4.65031141781114));
#36673=CARTESIAN_POINT('Ctrl Pts',(12.9511154303622,-0.336107011072318,
4.55759164674784));
#36674=CARTESIAN_POINT('Ctrl Pts',(12.974729546512,-0.56049590900091,4.33124115596169));
#36675=CARTESIAN_POINT('Ctrl Pts',(12.9983436626619,-0.650558060547343,
4.02550641626558));
#36676=CARTESIAN_POINT('Ctrl Pts',(13.0219577788117,-0.584709444123524,
3.71365888635357));
#36677=CARTESIAN_POINT('Ctrl Pts',(13.0455718949616,-0.378731139057797,
3.47043499764384));
#36678=CARTESIAN_POINT('Ctrl Pts',(13.0691860111115,-0.0819872800401352,
3.35412504823007));
#36679=CARTESIAN_POINT('Ctrl Pts',(13.0928001272613,0.234405401379786,3.39260352716186));
#36680=CARTESIAN_POINT('Ctrl Pts',(13.1164142434112,0.494621196584012,3.57664879910166));
#36681=CARTESIAN_POINT('Ctrl Pts',(13.1400283595611,0.636297578801308,3.86215313342763));
#36682=CARTESIAN_POINT('Ctrl Pts',(13.1636424757109,0.625480816776257,4.18069342892634));
#36683=CARTESIAN_POINT('Ctrl Pts',(13.1872565918608,0.464763222827219,4.45592928631477));
#36684=CARTESIAN_POINT('Ctrl Pts',(13.2108707080107,0.192661887153653,4.62189851635989));
#36685=CARTESIAN_POINT('Ctrl Pts',(13.2344848241605,-0.125612210960856,
4.63882543771344));
#36686=CARTESIAN_POINT('Ctrl Pts',(13.2580989403104,-0.413782468289504,
4.50265339583901));
#36687=CARTESIAN_POINT('Ctrl Pts',(13.2817130564603,-0.602786876612853,
4.24601696851145));
#36688=CARTESIAN_POINT('Ctrl Pts',(13.3053271726101,-0.647329213752593,
3.9304208620728));
#36689=CARTESIAN_POINT('Ctrl Pts',(13.32894128876,-0.536734598538914,3.6314998804023));
#36690=CARTESIAN_POINT('Ctrl Pts',(13.3525554049099,-0.297507800394296,
3.42089251764738));
#36691=CARTESIAN_POINT('Ctrl Pts',(13.3761695210598,0.0130188131672444,
3.34907229440132));
#36692=CARTESIAN_POINT('Ctrl Pts',(13.3997836372096,0.320425377524893,3.43325142712992));
#36693=CARTESIAN_POINT('Ctrl Pts',(13.4233977533595,0.551039769569266,3.65325580067535));
#36694=CARTESIAN_POINT('Ctrl Pts',(13.4470118695093,0.649593644862141,3.95635983539258));
#36695=CARTESIAN_POINT('Ctrl Pts',(13.4706259856592,0.592467881122722,4.26992253935193));
#36696=CARTESIAN_POINT('Ctrl Pts',(13.4942401018091,0.393353065302923,4.5187964277335));
#36697=CARTESIAN_POINT('Ctrl Pts',(13.5178542179589,0.0999684491195412,
4.64333714069132));
#36698=CARTESIAN_POINT('Ctrl Pts',(13.5414683341088,-0.217374301809525,
4.61369762939502));
#36699=CARTESIAN_POINT('Ctrl Pts',(13.5650824502587,-0.482621788093898,
4.43698120905743));
#36700=CARTESIAN_POINT('Ctrl Pts',(13.5886965664085,-0.632205603168059,
4.15553919999523));
#36701=CARTESIAN_POINT('Ctrl Pts',(13.6123106825584,-0.630276944445953,
3.83682113889318));
#36702=CARTESIAN_POINT('Ctrl Pts',(13.6359247987083,-0.477298028416376,
3.55721002779864));
#36703=CARTESIAN_POINT('Ctrl Pts',(13.6595389148582,-0.209931317243796,
3.38371661595291));
#36704=CARTESIAN_POINT('Ctrl Pts',(13.683153031008,0.107746895509167,3.35791980725116));
#36705=CARTESIAN_POINT('Ctrl Pts',(13.7067671471579,0.399602814690774,3.48600198647908));
#36706=CARTESIAN_POINT('Ctrl Pts',(13.7303812633077,0.59569113756138,3.73726736776131));
#36707=CARTESIAN_POINT('Ctrl Pts',(13.7539953794576,0.649017932507905,4.05149845333026));
#36708=CARTESIAN_POINT('Ctrl Pts',(13.7776094956075,0.546803061895555,4.35338757606046));
#36709=CARTESIAN_POINT('Ctrl Pts',(13.8012236117573,0.313543031018869,4.57058490613733));
#36710=CARTESIAN_POINT('Ctrl Pts',(13.8248377279072,0.00514023007941788,
4.65103759142385));
#36711=CARTESIAN_POINT('Ctrl Pts',(13.8484518440571,-0.304494462781446,
4.57546458583277));
#36712=CARTESIAN_POINT('Ctrl Pts',(13.8720659602069,-0.541154937947787,
4.36197748624323));
#36713=CARTESIAN_POINT('Ctrl Pts',(13.8956800763568,-0.648123865072376,
4.06173996222779));
#36714=CARTESIAN_POINT('Ctrl Pts',(13.9192941925067,-0.599765396122921,
3.74670602647169));
#36715=CARTESIAN_POINT('Ctrl Pts',(13.9429083086565,-0.407668974822819,
3.49237575473668));
#36716=CARTESIAN_POINT('Ctrl Pts',(13.9665224248064,-0.117871845784803,
3.35970116712309));
#36717=CARTESIAN_POINT('Ctrl Pts',(13.9901365409563,0.200174091641329,3.38047865214521));
#36718=CARTESIAN_POINT('Ctrl Pts',(14.0137506571061,0.470246914526057,3.54972874087838));
#36719=CARTESIAN_POINT('Ctrl Pts',(14.037364773256,0.627621790796785,3.82688947135059));
#36720=CARTESIAN_POINT('Ctrl Pts',(14.0609788894059,0.634582735815489,4.14553734509456));
#36721=CARTESIAN_POINT('Ctrl Pts',(14.0845930055557,0.489461510650943,4.42930618095194));
#36722=CARTESIAN_POINT('Ctrl Pts',(14.1082071217056,0.227037427151766,4.61018880199865));
#36723=CARTESIAN_POINT('Ctrl Pts',(14.1318212378555,-0.0897977562486571,
4.64483542891575));
#36724=CARTESIAN_POINT('Ctrl Pts',(14.1554353540053,-0.385112282251534,
4.52494275637564));
#36725=CARTESIAN_POINT('Ctrl Pts',(14.1790494701552,-0.588131968915973,
4.27924389796604));
#36726=CARTESIAN_POINT('Ctrl Pts',(14.2026635863051,-0.65020173504413,3.96662229549764));
#36727=CARTESIAN_POINT('Ctrl Pts',(14.2262777024549,-0.556446129094758,
3.66199989226673));
#36728=CARTESIAN_POINT('Ctrl Pts',(14.2498918186048,-0.329334334698108,
3.43838156778717));
#36729=CARTESIAN_POINT('Ctrl Pts',(14.2735059347547,-0.0232952743833569,
3.34935901020328));
#36730=CARTESIAN_POINT('Ctrl Pts',(14.2971200509045,0.28832666060365,3.41626709515619));
#36731=CARTESIAN_POINT('Ctrl Pts',(14.3207341670544,0.530849104237583,3.62307083431711));
#36732=CARTESIAN_POINT('Ctrl Pts',(14.3443482832043,0.646149864620809,3.92020827196535));
#36733=CARTESIAN_POINT('Ctrl Pts',(14.3679623993541,0.606596311879891,4.2364683526943));
#36734=CARTESIAN_POINT('Ctrl Pts',(14.391576515504,0.42166773027486,4.49605714656388));
#36735=CARTESIAN_POINT('Ctrl Pts',(14.4151906316539,0.135683541737747,4.63676239203782));
#36736=CARTESIAN_POINT('Ctrl Pts',(14.4388047478037,-0.182818152115814,
4.62486309754155));
#36737=CARTESIAN_POINT('Ctrl Pts',(14.4624188639536,-0.457506203155893,
4.46321101183598));
#36738=CARTESIAN_POINT('Ctrl Pts',(14.4860329801035,-0.622549707754089,
4.19054718257559));
#36739=CARTESIAN_POINT('Ctrl Pts',(14.5096470962533,-0.63839484111024,3.87221739454711));
#36740=CARTESIAN_POINT('Ctrl Pts',(14.5332612124032,-0.501244206711231,
3.58451159745434));
#36741=CARTESIAN_POINT('Ctrl Pts',(14.5568753285531,-0.243966908844842,
3.39638048838484));
#36742=CARTESIAN_POINT('Ctrl Pts',(14.5804894447029,0.0717787570654544,
3.35291099727801));
#36743=CARTESIAN_POINT('Ctrl Pts',(14.6041035608528,0.370322144162233,3.46452089026927));
#36744=CARTESIAN_POINT('Ctrl Pts',(14.6277176770027,0.580115251486915,3.70446207957941));
#36745=CARTESIAN_POINT('Ctrl Pts',(14.6513317931525,0.650879700384091,4.0152309888134));
#36746=CARTESIAN_POINT('Ctrl Pts',(14.6749459093024,0.565656298155129,4.32234968564526));
#36747=CARTESIAN_POINT('Ctrl Pts',(14.6985600254523,0.344869426209941,4.55221503612336));
#36748=CARTESIAN_POINT('Ctrl Pts',(14.7221741416021,0.041432195817608,4.64973820947522));
#36749=CARTESIAN_POINT('Ctrl Pts',(14.745788257752,-0.271934549361806,4.59154709694401));
#36750=CARTESIAN_POINT('Ctrl Pts',(14.7694023739019,-0.520130285395982,
4.39158760667368));
#36751=CARTESIAN_POINT('Ctrl Pts',(14.7930164900517,-0.64367318065081,4.09778141619902));
#36752=CARTESIAN_POINT('Ctrl Pts',(14.8166306062016,-0.612955311082805,
3.78054123783642));
#36753=CARTESIAN_POINT('Ctrl Pts',(14.8402447223515,-0.435338447621071,
3.51589585985611));
#36754=CARTESIAN_POINT('Ctrl Pts',(14.8638588385013,-0.153389665944836,
3.36726945127358));
#36755=CARTESIAN_POINT('Ctrl Pts',(14.8874729546512,0.165319955489652,3.37028123293502));
#36756=CARTESIAN_POINT('Ctrl Pts',(14.9110870708011,0.444409630539555,3.52420969451069));
#36757=CARTESIAN_POINT('Ctrl Pts',(14.9347011869509,0.616993161964042,3.79216419995926));
#36758=CARTESIAN_POINT('Ctrl Pts',(14.9583153031008,0.641710593195818,4.10992889087348));
#36759=CARTESIAN_POINT('Ctrl Pts',(14.9819294192507,0.512636325700993,4.40134645341462));
#36760=CARTESIAN_POINT('Ctrl Pts',(15.0055435354005,0.260708010403211,4.59658262768273));
#36761=CARTESIAN_POINT('Ctrl Pts',(15.0291576515504,-0.0537065278721878,
4.64883488988255));
#36762=CARTESIAN_POINT('Ctrl Pts',(15.0527717677003,-0.355236031271534,
4.54560815721762));
#36763=CARTESIAN_POINT('Ctrl Pts',(15.0763858838501,-0.571652475026301,
4.31158258982903));
#36764=CARTESIAN_POINT('Ctrl Pts',(15.09212862795,-0.624530364890795,4.10584538053252));
#36765=CARTESIAN_POINT('Ctrl Pts',(15.1,-0.624993681275899,4.00281040303152));
#36766=CARTESIAN_POINT('Ctrl Pts',(15.1,-0.624993681275899,4.00281040303152));
#36767=CARTESIAN_POINT('Ctrl Pts',(15.1,-0.617358358083874,4.02914127082806));
#36768=CARTESIAN_POINT('Ctrl Pts',(15.1,-0.607931963506944,4.05484759228836));
#36769=CARTESIAN_POINT('Ctrl Pts',(15.1,-0.596773861259576,4.07974656001827));
#36770=CARTESIAN_POINT('Ctrl Pts',(15.1,-0.585871522029423,4.10407480030985));
#36771=CARTESIAN_POINT('Ctrl Pts',(15.1,-0.573314772633929,4.12763281365198));
#36772=CARTESIAN_POINT('Ctrl Pts',(15.1,-0.559143639302279,4.1502040881484));
#36773=CARTESIAN_POINT('Ctrl Pts',(15.1,-0.549626121151564,4.16536325076984));
#36774=CARTESIAN_POINT('Ctrl Pts',(15.1,-0.539380106047495,4.18007635520315));
#36775=CARTESIAN_POINT('Ctrl Pts',(15.1,-0.528417753985571,4.19426420824267));
#36776=CARTESIAN_POINT('Ctrl Pts',(15.1,-0.523814643226911,4.2002217124899));
#36777=CARTESIAN_POINT('Ctrl Pts',(15.1,-0.519084627089791,4.20608691507751));
#36778=CARTESIAN_POINT('Ctrl Pts',(15.1,-0.514239086396905,4.21184190560023));
#36779=CARTESIAN_POINT('Ctrl Pts',(15.1,-0.50085552272952,4.2277374035328));
#36780=CARTESIAN_POINT('Ctrl Pts',(15.1,-0.486572803760524,4.24281789068328));
#36781=CARTESIAN_POINT('Ctrl Pts',(15.1,-0.4714177983537,4.25697008589974));
#36782=CARTESIAN_POINT('Ctrl Pts',(15.1,-0.457151696655403,4.27029219637033));
#36783=CARTESIAN_POINT('Ctrl Pts',(15.1,-0.442112042545397,4.28279146400573));
#36784=CARTESIAN_POINT('Ctrl Pts',(15.1,-0.426369607892924,4.29437520287289));
#36785=CARTESIAN_POINT('Ctrl Pts',(15.1,-0.419074661497203,4.29974303548351));
#36786=CARTESIAN_POINT('Ctrl Pts',(15.1,-0.411628924918527,4.30491398987477));
#36787=CARTESIAN_POINT('Ctrl Pts',(15.1,-0.404040271526401,4.30987739070861));
#36788=CARTESIAN_POINT('Ctrl Pts',(15.1,-0.398073367501634,4.31378007737535));
#36789=CARTESIAN_POINT('Ctrl Pts',(15.1,-0.392026704362881,4.31754881952869));
#36790=CARTESIAN_POINT('Ctrl Pts',(15.1,-0.385904261325812,4.32117966642505));
#36791=CARTESIAN_POINT('Ctrl Pts',(15.1,-0.366868686798561,4.33246850264191));
#36792=CARTESIAN_POINT('Ctrl Pts',(15.1,-0.347097727375919,4.34242824684389));
#36793=CARTESIAN_POINT('Ctrl Pts',(15.1,-0.326713262272485,4.3509180109496));
#36794=CARTESIAN_POINT('Ctrl Pts',(15.1,-0.308010762698638,4.35870726657947));
#36795=CARTESIAN_POINT('Ctrl Pts',(15.1,-0.288791261952878,4.36525839133365));
#36796=CARTESIAN_POINT('Ctrl Pts',(15.1,-0.269173508333929,4.37043259773196));
#36797=CARTESIAN_POINT('Ctrl Pts',(12.5,-0.186196943290592,3.58169363627332));
#36798=CARTESIAN_POINT('Ctrl Pts',(12.5,-0.170588484282379,3.56594316788148));
#36799=CARTESIAN_POINT('Ctrl Pts',(12.5,-0.153797667832464,3.55144458439849));
#36800=CARTESIAN_POINT('Ctrl Pts',(12.5,-0.136060690067392,3.53823162417247));
#36801=CARTESIAN_POINT('Ctrl Pts',(12.5,-0.117990710310259,3.5247705978929));
#36802=CARTESIAN_POINT('Ctrl Pts',(12.5,-0.0989385549429972,3.51264262455394));
#36803=CARTESIAN_POINT('Ctrl Pts',(12.5,-0.0790990435859813,3.5018744512649));
#36804=CARTESIAN_POINT('Ctrl Pts',(12.5,-0.0668145727052721,3.49520688224936));
#36805=CARTESIAN_POINT('Ctrl Pts',(12.5,-0.054227138249592,3.4890605701039));
#36806=CARTESIAN_POINT('Ctrl Pts',(12.5,-0.0413735013057162,3.4834433907237));
#36807=CARTESIAN_POINT('Ctrl Pts',(12.5,-0.0353493612034326,3.48081077586818));
#36808=CARTESIAN_POINT('Ctrl Pts',(12.5,-0.0292710672153644,3.47829647656688));
#36809=CARTESIAN_POINT('Ctrl Pts',(12.5,-0.0231507758853709,3.47590397706369));
#36810=CARTESIAN_POINT('Ctrl Pts',(12.5,-0.00211397253512804,3.467680423829));
#36811=CARTESIAN_POINT('Ctrl Pts',(12.5,0.0194422610390746,3.46088402724794));
#36812=CARTESIAN_POINT('Ctrl Pts',(12.5,0.0413436963816045,3.45552737346533));
#36813=CARTESIAN_POINT('Ctrl Pts',(12.5,0.0650920698750741,3.44971899548849));
#36814=CARTESIAN_POINT('Ctrl Pts',(12.5,0.089246474293393,3.44560199012534));
#36815=CARTESIAN_POINT('Ctrl Pts',(12.5,0.113633446029948,3.44311473184586));
#36816=CARTESIAN_POINT('Ctrl Pts',(12.5,0.123118497624279,3.44214733936417));
#36817=CARTESIAN_POINT('Ctrl Pts',(12.5,0.132642564327611,3.44142688205345));
#36818=CARTESIAN_POINT('Ctrl Pts',(12.5,0.142169452875131,3.44095138714122));
#36819=CARTESIAN_POINT('Ctrl Pts',(12.5,0.170359862108328,3.43954438042575));
#36820=CARTESIAN_POINT('Ctrl Pts',(12.5,0.19861482332424,3.44027367679077));
#36821=CARTESIAN_POINT('Ctrl Pts',(12.5,0.226679319731597,3.44302987267532));
#36822=CARTESIAN_POINT('Ctrl Pts',(12.5,0.254743816138955,3.44578606855986));
#36823=CARTESIAN_POINT('Ctrl Pts',(12.5,0.282619254593541,3.45056842907764));
#36824=CARTESIAN_POINT('Ctrl Pts',(12.5,0.310093463203745,3.45730861053194));
#36825=CARTESIAN_POINT('Ctrl Pts',(15.0699957084852,-1.05870731373636E-5,
4.45788944868556));
#36826=CARTESIAN_POINT('Ctrl Pts',(15.0634386537186,0.0628625045491076,
4.45782850550181));
#36827=CARTESIAN_POINT('Ctrl Pts',(15.0568815989521,0.125761012144406,4.44477074790967));
#36828=CARTESIAN_POINT('Ctrl Pts',(15.0503245441856,0.183365120595825,4.41959809737683));
#36829=CARTESIAN_POINT('Ctrl Pts',(15.0424531721356,0.252515583017112,4.38937975928409));
#36830=CARTESIAN_POINT('Ctrl Pts',(15.0345818000857,0.314036477612831,4.34170308552782));
#36831=CARTESIAN_POINT('Ctrl Pts',(15.0267104280357,0.360556892971808,4.28228266426341));
#36832=CARTESIAN_POINT('Ctrl Pts',(15.0188390559858,0.407077308330786,4.222862242999));
#36833=CARTESIAN_POINT('Ctrl Pts',(15.0109676839358,0.438597244453022,4.15169807422645));
#36834=CARTESIAN_POINT('Ctrl Pts',(15.0030963118859,0.45133921416074,4.07731692107955));
#36835=CARTESIAN_POINT('Ctrl Pts',(14.9952249398359,0.464081183868457,4.00293576793266));
#36836=CARTESIAN_POINT('Ctrl Pts',(14.9873535677859,0.458045187161657,3.92533763041141));
#36837=CARTESIAN_POINT('Ctrl Pts',(14.979482195736,0.433954739621328,3.85382131653551));
#36838=CARTESIAN_POINT('Ctrl Pts',(14.971610823686,0.409864292080999,3.78230500265962));
#36839=CARTESIAN_POINT('Ctrl Pts',(14.9637394516361,0.367719393707138,3.71687051242907));
#36840=CARTESIAN_POINT('Ctrl Pts',(14.9558680795861,0.312570095196614,3.66535860215541));
#36841=CARTESIAN_POINT('Ctrl Pts',(14.9479967075362,0.257420796686091,3.61384669188175));
#36842=CARTESIAN_POINT('Ctrl Pts',(14.9401253354862,0.189267098038905,3.57625736156498));
#36843=CARTESIAN_POINT('Ctrl Pts',(14.9322539634362,0.116275803938161,3.55709495786573));
#36844=CARTESIAN_POINT('Ctrl Pts',(14.9243825913863,0.0432845098374172,
3.53793255416647));
#36845=CARTESIAN_POINT('Ctrl Pts',(14.9165112193363,-0.0345443797168851,
3.53719707708475));
#36846=CARTESIAN_POINT('Ctrl Pts',(14.9086398472864,-0.107884770736704,
3.55497662303181));
#36847=CARTESIAN_POINT('Ctrl Pts',(14.9007684752364,-0.181225161756525,
3.57275616897888));
#36848=CARTESIAN_POINT('Ctrl Pts',(14.8928971031865,-0.250077054241862,
3.60905073795473));
#36849=CARTESIAN_POINT('Ctrl Pts',(14.8850257311365,-0.306190019513209,
3.65951122309406));
#36850=CARTESIAN_POINT('Ctrl Pts',(14.8771543590866,-0.362302984784554,
3.70997170823338));
#36851=CARTESIAN_POINT('Ctrl Pts',(14.8692829870366,-0.405677022841909,
3.77459810953617));
#36852=CARTESIAN_POINT('Ctrl Pts',(14.8614116149867,-0.431114693744839,
3.84564633596564));
#36853=CARTESIAN_POINT('Ctrl Pts',(14.8535402429367,-0.45655236464777,3.91669456239511));
#36854=CARTESIAN_POINT('Ctrl Pts',(14.8456688708867,-0.464053668396277,
3.99416461395126));
#36855=CARTESIAN_POINT('Ctrl Pts',(14.8377974988368,-0.452719732759917,
4.06877337558629));
#36856=CARTESIAN_POINT('Ctrl Pts',(14.8299261267868,-0.441385797123556,
4.14338213722132));
#36857=CARTESIAN_POINT('Ctrl Pts',(14.8220547547369,-0.411216622102327,
4.21512960893523));
#36858=CARTESIAN_POINT('Ctrl Pts',(14.8141833826869,-0.365827335221939,
4.27541839855419));
#36859=CARTESIAN_POINT('Ctrl Pts',(14.806312010637,-0.32043804834155,4.33570718817315));
#36860=CARTESIAN_POINT('Ctrl Pts',(14.798440638587,-0.259828649602004,4.38453729569717));
#36861=CARTESIAN_POINT('Ctrl Pts',(14.7905692665371,-0.191261870645823,
4.41605748429924));
#36862=CARTESIAN_POINT('Ctrl Pts',(14.7837114138531,-0.131523763221734,
4.44351912740692));
#36863=CARTESIAN_POINT('Ctrl Pts',(14.7768535611691,-0.065745536276614,
4.45784152413683));
#36864=CARTESIAN_POINT('Ctrl Pts',(14.7699957084852,8.6346448269735E-6,
4.45789857801605));
#36865=CARTESIAN_POINT('Ctrl Pts',(12.5,0.310062960217722,4.54266560670548));
#36866=CARTESIAN_POINT('Ctrl Pts',(12.50787137205,0.220600394030941,4.59378185169648));
#36867=CARTESIAN_POINT('Ctrl Pts',(12.5236141161499,0.0159878432799406,
4.65085692712531));
#36868=CARTESIAN_POINT('Ctrl Pts',(12.5472282322997,-0.294892507759568,
4.580447501361));
#36869=CARTESIAN_POINT('Ctrl Pts',(12.5708423484496,-0.535054221536356,
4.37092866956447));
#36870=CARTESIAN_POINT('Ctrl Pts',(12.5944564645995,-0.647009713430093,
4.07251155115386));
#36871=CARTESIAN_POINT('Ctrl Pts',(12.6180705807493,-0.603894380709874,
3.75671714932517));
#36872=CARTESIAN_POINT('Ctrl Pts',(12.6416846968992,-0.416056506175611,
3.49922677321964));
#36873=CARTESIAN_POINT('Ctrl Pts',(12.6652988130491,-0.128505496873939,
3.36175035317655));
#36874=CARTESIAN_POINT('Ctrl Pts',(12.6889129291989,0.189841674427298,3.37723482234205));
#36875=CARTESIAN_POINT('Ctrl Pts',(12.7125270453488,0.462692468193658,3.54196933898577));
#36876=CARTESIAN_POINT('Ctrl Pts',(12.7361411614987,0.624655556881011,3.81647407445394));
#36877=CARTESIAN_POINT('Ctrl Pts',(12.7597552776485,0.636915702199809,4.13496208375113));
#36878=CARTESIAN_POINT('Ctrl Pts',(12.7833693937984,0.496534514683115,4.42110548633398));
#36879=CARTESIAN_POINT('Ctrl Pts',(12.8069835099483,0.237155397994168,4.60632802944461));
#36880=CARTESIAN_POINT('Ctrl Pts',(12.8305976260981,-0.0790596718614395,
4.64623983861064));
#36881=CARTESIAN_POINT('Ctrl Pts',(12.854211742248,-0.376327535803878,4.5312757721487));
#36882=CARTESIAN_POINT('Ctrl Pts',(12.8778258583979,-0.583405888470749,
4.28898776831928));
#36883=CARTESIAN_POINT('Ctrl Pts',(12.9014399745477,-0.650666957548692,
3.97744183415536));
#36884=CARTESIAN_POINT('Ctrl Pts',(12.9250540906976,-0.561991161265395,
3.67130212143154));
#36885=CARTESIAN_POINT('Ctrl Pts',(12.9486682068475,-0.338630270727757,
3.44393714350224));
#36886=CARTESIAN_POINT('Ctrl Pts',(12.9722823229973,-0.0341142786054444,
3.34983650006563));
#36887=CARTESIAN_POINT('Ctrl Pts',(12.9958964391472,0.278577437919422,3.41155206540036));
#36888=CARTESIAN_POINT('Ctrl Pts',(13.0195105552971,0.524506132150044,3.61429327464512));
#36889=CARTESIAN_POINT('Ctrl Pts',(13.0431246714469,0.644733280558021,3.90947178565704));
#36890=CARTESIAN_POINT('Ctrl Pts',(13.0667387875968,0.61044561006836,4.22634601343335));
#36891=CARTESIAN_POINT('Ctrl Pts',(13.0903529037467,0.429860399609997,4.4889748434194));
#36892=CARTESIAN_POINT('Ctrl Pts',(13.1139670198965,0.146256151980267,4.63441744826062));
#36893=CARTESIAN_POINT('Ctrl Pts',(13.1375811360464,-0.172399400609521,
4.62781749523177));
#36894=CARTESIAN_POINT('Ctrl Pts',(13.1611952521963,-0.449738236712957,
4.47075670902068));
#36895=CARTESIAN_POINT('Ctrl Pts',(13.1848093683461,-0.619294173608025,
4.2008758003961));
#36896=CARTESIAN_POINT('Ctrl Pts',(13.208423484496,-0.64043195068177,3.88285360784221));
#36897=CARTESIAN_POINT('Ctrl Pts',(13.2320376006459,-0.508085752511173,
3.59290636366459));
#36898=CARTESIAN_POINT('Ctrl Pts',(13.2556517167957,-0.253973266794505,
3.40052194335125));
#36899=CARTESIAN_POINT('Ctrl Pts',(13.2792658329456,0.0610056803032868,
3.3518066124833));
#36900=CARTESIAN_POINT('Ctrl Pts',(13.3028799490955,0.361364191435218,3.45843533922715));
#36901=CARTESIAN_POINT('Ctrl Pts',(13.3264940652453,0.575119258511334,3.69485380694));
#36902=CARTESIAN_POINT('Ctrl Pts',(13.3501081813952,0.65104299168552,4.00440268404554));
#36903=CARTESIAN_POINT('Ctrl Pts',(13.3737222975451,0.570939739771795,4.31289642727099));
#36904=CARTESIAN_POINT('Ctrl Pts',(13.3973364136949,0.354006804717113,4.54640236352309));
#36905=CARTESIAN_POINT('Ctrl Pts',(13.4209505298448,0.0522336745508671,
4.6489591696652));
#36906=CARTESIAN_POINT('Ctrl Pts',(13.4445646459947,-0.26205761933777,4.59598839317277));
#36907=CARTESIAN_POINT('Ctrl Pts',(13.4681787621445,-0.513544980480383,
4.40018484937968));
#36908=CARTESIAN_POINT('Ctrl Pts',(13.4917928782944,-0.64195771209056,4.10847422061066));
#36909=CARTESIAN_POINT('Ctrl Pts',(13.5154069944443,-0.616520809113462,
3.79076698974655));
#36910=CARTESIAN_POINT('Ctrl Pts',(13.5390211105941,-0.443330402422436,
3.52320390633144));
#36911=CARTESIAN_POINT('Ctrl Pts',(13.562635226744,-0.163892778617988,3.36990832590288));
#36912=CARTESIAN_POINT('Ctrl Pts',(13.5862493428939,0.154822890495328,3.36761860145296));
#36913=CARTESIAN_POINT('Ctrl Pts',(13.6098634590437,0.43643417612693,3.51688348138565));
#36914=CARTESIAN_POINT('Ctrl Pts',(13.6334775751936,0.613450973283793,3.78193059814177));
#36915=CARTESIAN_POINT('Ctrl Pts',(13.6570916913435,0.643449974253473,4.09923956510808));
#36916=CARTESIAN_POINT('Ctrl Pts',(13.6807058074933,0.519241709620395,4.39276507945606));
#36917=CARTESIAN_POINT('Ctrl Pts',(13.7043199236432,0.270593554659618,4.59216170834183));
#36918=CARTESIAN_POINT('Ctrl Pts',(13.7279340397931,-0.0429042293685969,
4.64964266158552));
#36919=CARTESIAN_POINT('Ctrl Pts',(13.7515481559429,-0.346119716157775,
4.55143222859795));
#36920=CARTESIAN_POINT('Ctrl Pts',(13.7751622720928,-0.566385203513325,
4.32106722332061));
#36921=CARTESIAN_POINT('Ctrl Pts',(13.7987763882427,-0.650912534047929,
4.01375622291695));
#36922=CARTESIAN_POINT('Ctrl Pts',(13.8223905043925,-0.57944414457563,3.70314844792952));
#36923=CARTESIAN_POINT('Ctrl Pts',(13.8460046205424,-0.369107932149097,
3.46368321387984));
#36924=CARTESIAN_POINT('Ctrl Pts',(13.8696187366923,-0.0703124342978696,
3.35275003110641));
#36925=CARTESIAN_POINT('Ctrl Pts',(13.8932328528421,0.245333927901481,3.3969348091043));
#36926=CARTESIAN_POINT('Ctrl Pts',(13.916846968992,0.502184306426786,3.58564835824111));
#36927=CARTESIAN_POINT('Ctrl Pts',(13.9404610851419,0.638682720042094,3.87366416276737));
#36928=CARTESIAN_POINT('Ctrl Pts',(13.9640752012917,0.62211637371287,4.19195723015293));
#36929=CARTESIAN_POINT('Ctrl Pts',(13.9876893174416,0.456455507660852,4.46424641105313));
#36930=CARTESIAN_POINT('Ctrl Pts',(14.0113034335915,0.181401901656729,4.62527570776815));
#36931=CARTESIAN_POINT('Ctrl Pts',(14.0349175497413,-0.137125932879425,
4.63645332836083));
#36932=CARTESIAN_POINT('Ctrl Pts',(14.0585316658912,-0.422790583021024,
4.49510047824495));
#36933=CARTESIAN_POINT('Ctrl Pts',(14.0821457820411,-0.60713052675338,4.23509335195577));
#36934=CARTESIAN_POINT('Ctrl Pts',(14.1057598981909,-0.645967413308333,
3.91874446730605));
#36935=CARTESIAN_POINT('Ctrl Pts',(14.1293740143408,-0.529993712466286,
3.62186903671368));
#36936=CARTESIAN_POINT('Ctrl Pts',(14.1529881304907,-0.287003328966194,
3.41561532377041));
#36937=CARTESIAN_POINT('Ctrl Pts',(14.1766022466405,0.0247694002478971,
3.34941346658496));
#36938=CARTESIAN_POINT('Ctrl Pts',(14.2002163627904,0.330605970264406,3.43912920108534));
#36939=CARTESIAN_POINT('Ctrl Pts',(14.2238304789403,0.557210518047066,3.66326152695696));
#36940=CARTESIAN_POINT('Ctrl Pts',(14.2474445950901,0.650275686248857,3.96809557204375));
#36941=CARTESIAN_POINT('Ctrl Pts',(14.27105871124,0.587497759452106,4.28057573538778));
#36942=CARTESIAN_POINT('Ctrl Pts',(14.2946728273899,0.383921904832036,4.52581397056352));
#36943=CARTESIAN_POINT('Ctrl Pts',(14.3182869435397,0.088336493108731,4.64503722732482));
#36944=CARTESIAN_POINT('Ctrl Pts',(14.3419010596896,-0.22841937412829,4.6096728222354));
#36945=CARTESIAN_POINT('Ctrl Pts',(14.3655151758395,-0.490432948250941,
4.42819608115853));
#36946=CARTESIAN_POINT('Ctrl Pts',(14.3891292919893,-0.634910852255616,
4.14409916841427));
#36947=CARTESIAN_POINT('Ctrl Pts',(14.4127434081392,-0.627227950688033,
3.82546788683648));
#36948=CARTESIAN_POINT('Ctrl Pts',(14.4363575242891,-0.469225504392149,
3.54866444115539));
#36949=CARTESIAN_POINT('Ctrl Pts',(14.4599716404389,-0.198769899531221,
3.38002670405092));
#36950=CARTESIAN_POINT('Ctrl Pts',(14.4835857565888,0.11932229545683,3.35996988316441));
#36951=CARTESIAN_POINT('Ctrl Pts',(14.5071998727387,0.408818071695872,3.49330073524378));
#36952=CARTESIAN_POINT('Ctrl Pts',(14.5308139888885,0.600337751131954,3.74806559342675));
#36953=CARTESIAN_POINT('Ctrl Pts',(14.5544281050384,0.647982309355475,4.06320828594604));
#36954=CARTESIAN_POINT('Ctrl Pts',(14.5780422211883,0.540333396317157,4.36320267272319));
#36955=CARTESIAN_POINT('Ctrl Pts',(14.6016563373381,0.303189823409542,4.57615301060753));
#36956=CARTESIAN_POINT('Ctrl Pts',(14.625270453488,-0.00661530128860875,
4.65102426869959));
#36957=CARTESIAN_POINT('Ctrl Pts',(14.6488845696379,-0.314835022974042,
4.56987302880665));
#36958=CARTESIAN_POINT('Ctrl Pts',(14.6724986857877,-0.547602339746838,
4.35214775046202));
#36959=CARTESIAN_POINT('Ctrl Pts',(14.6961128019376,-0.649132943719538,
4.05002781234082));
#36960=CARTESIAN_POINT('Ctrl Pts',(14.7197269180875,-0.595094318970103,
3.73591836064326));
#36961=CARTESIAN_POINT('Ctrl Pts',(14.7433410342373,-0.398437197867616,
3.48509791236843));
#36962=CARTESIAN_POINT('Ctrl Pts',(14.7669551503872,-0.1062918289807,3.35767733339665));
#36963=CARTESIAN_POINT('Ctrl Pts',(14.7905692665371,0.211327117384507,3.38419385377023));
#36964=CARTESIAN_POINT('Ctrl Pts',(14.8141833826869,0.478300047385911,3.5582926020622));
#36965=CARTESIAN_POINT('Ctrl Pts',(14.8377974988368,0.630645044771057,3.83824960712979));
#36966=CARTESIAN_POINT('Ctrl Pts',(14.8614116149867,0.631851559871185,4.15697121131127));
#36967=CARTESIAN_POINT('Ctrl Pts',(14.8850257311365,0.481630465478622,4.4380735902585));
#36968=CARTESIAN_POINT('Ctrl Pts',(14.9086398472864,0.215983244330552,4.61418854455152));
#36969=CARTESIAN_POINT('Ctrl Pts',(14.9322539634363,-0.101425794369151,
4.64310902247508));
#36970=CARTESIAN_POINT('Ctrl Pts',(14.9558680795861,-0.394527586443172,
4.517903766532));
#36971=CARTESIAN_POINT('Ctrl Pts',(14.979482195736,-0.593077772790822,4.26857965265179));
#36972=CARTESIAN_POINT('Ctrl Pts',(15.0030963118859,-0.649493436571599,
3.95488773069898));
#36973=CARTESIAN_POINT('Ctrl Pts',(15.0267104280357,-0.550252000240565,
3.65200904506483));
#36974=CARTESIAN_POINT('Ctrl Pts',(15.0503245441856,-0.319142060764588,
3.43252503194012));
#36975=CARTESIAN_POINT('Ctrl Pts',(15.0739386603355,-0.0115409051696555,
3.34904846156061));
#36976=CARTESIAN_POINT('Ctrl Pts',(15.0975527764853,0.298810377697559,3.42155963907315));
#36977=CARTESIAN_POINT('Ctrl Pts',(15.1211668926352,0.537575400322941,3.63273573589665));
#36978=CARTESIAN_POINT('Ctrl Pts',(15.1369096367351,0.610790903144771,3.83214323401692));
#36979=CARTESIAN_POINT('Ctrl Pts',(15.1447810087851,0.621570310124627,3.93461384266089));
#36980=CARTESIAN_POINT('Ctrl Pts',(12.4850729970716,0.282426015030316,4.49429601229446));
#36981=CARTESIAN_POINT('Ctrl Pts',(12.4929443691216,0.200937545576316,4.54085609598193));
#36982=CARTESIAN_POINT('Ctrl Pts',(12.5086871132215,0.0145627935155885,
4.59284387968754));
#36983=CARTESIAN_POINT('Ctrl Pts',(12.5323012293714,-0.268607755567932,
4.52871028073968));
#36984=CARTESIAN_POINT('Ctrl Pts',(12.5559153455213,-0.487363055256749,
4.3378665608173));
#36985=CARTESIAN_POINT('Ctrl Pts',(12.5795294616711,-0.589339580973024,
4.06604835489435));
#36986=CARTESIAN_POINT('Ctrl Pts',(12.603143577821,-0.550067261575934,3.77840176074865));
#36987=CARTESIAN_POINT('Ctrl Pts',(12.6267576939709,-0.378972002925158,
3.54386236016666));
#36988=CARTESIAN_POINT('Ctrl Pts',(12.6503718101207,-0.117051373585908,
3.41863967169675));
#36989=CARTESIAN_POINT('Ctrl Pts',(12.6739859262706,0.172920453180012,3.43274395851062));
#36990=CARTESIAN_POINT('Ctrl Pts',(12.6976000424204,0.42145114619533,3.58279513857084));
#36991=CARTESIAN_POINT('Ctrl Pts',(12.7212141585703,0.568977924911017,3.83283235195095));
#36992=CARTESIAN_POINT('Ctrl Pts',(12.7448282747202,0.580145282610399,4.12293246335278));
#36993=CARTESIAN_POINT('Ctrl Pts',(12.76844239087,0.45227673827436,4.38357095065208));
#36994=CARTESIAN_POINT('Ctrl Pts',(12.7920565070199,0.216016946852954,4.55228399108678));
#36995=CARTESIAN_POINT('Ctrl Pts',(12.8156706231698,-0.0720128197761896,
4.58863832766248));
#36996=CARTESIAN_POINT('Ctrl Pts',(12.8392847393196,-0.34278420811256,4.48392139165784));
#36997=CARTESIAN_POINT('Ctrl Pts',(12.8628988554695,-0.531404976945056,
4.26322932523642));
#36998=CARTESIAN_POINT('Ctrl Pts',(12.8865129716194,-0.592670842732518,
3.97945251867098));
#36999=CARTESIAN_POINT('Ctrl Pts',(12.9101270877692,-0.51189901575794,3.70060005900794));
#37000=CARTESIAN_POINT('Ctrl Pts',(12.9337412039191,-0.308447025930223,
3.49350087944474));
#37001=CARTESIAN_POINT('Ctrl Pts',(12.957355320069,-0.0310735592390789,
3.40778774002645));
#37002=CARTESIAN_POINT('Ctrl Pts',(12.9809694362188,0.253746902286204,3.46400239130434));
#37003=CARTESIAN_POINT('Ctrl Pts',(13.0045835523687,0.477755152237737,3.64867260076509));
#37004=CARTESIAN_POINT('Ctrl Pts',(13.0281976685186,0.587266054150949,3.91754086716214));
#37005=CARTESIAN_POINT('Ctrl Pts',(13.0518117846685,0.556034558024266,4.20617103876933));
#37006=CARTESIAN_POINT('Ctrl Pts',(13.0754259008183,0.391545509324759,4.44539088570928));
#37007=CARTESIAN_POINT('Ctrl Pts',(13.0990400169682,0.133219853633759,4.57786970637232));
#37008=CARTESIAN_POINT('Ctrl Pts',(13.122654133118,-0.157032867368526,4.57185802915678));
#37009=CARTESIAN_POINT('Ctrl Pts',(13.1462682492679,-0.409651568547275,
4.42879659435664));
#37010=CARTESIAN_POINT('Ctrl Pts',(13.1698823654178,-0.564094419600429,
4.1829710707208));
#37011=CARTESIAN_POINT('Ctrl Pts',(13.1934964815676,-0.583348116144335,
3.89329525626321));
#37012=CARTESIAN_POINT('Ctrl Pts',(13.2171105977175,-0.462798375770677,
3.62919197644995));
#37013=CARTESIAN_POINT('Ctrl Pts',(13.2407247138674,-0.231335782947555,
3.45395542080054));
#37014=CARTESIAN_POINT('Ctrl Pts',(13.2643388300172,0.055568040665587,3.40958224975729));
#37015=CARTESIAN_POINT('Ctrl Pts',(13.2879529461671,0.329154596505292,3.50670680265737));
#37016=CARTESIAN_POINT('Ctrl Pts',(13.311567062317,0.523856961936024,3.72205250428141));
#37017=CARTESIAN_POINT('Ctrl Pts',(13.3351811784668,0.593013359693284,4.00401025814095));
#37018=CARTESIAN_POINT('Ctrl Pts',(13.3587952946167,0.520049977633468,4.28500692572024));
#37019=CARTESIAN_POINT('Ctrl Pts',(13.3824094107666,0.322452998189994,4.49769969952106));
#37020=CARTESIAN_POINT('Ctrl Pts',(13.4060235269164,0.0475779130258999,
4.59111527567571));
#37021=CARTESIAN_POINT('Ctrl Pts',(13.4296376430663,-0.238699550200797,
4.5428659610613));
#37022=CARTESIAN_POINT('Ctrl Pts',(13.4532517592162,-0.467771004553565,
4.36451503980497));
#37023=CARTESIAN_POINT('Ctrl Pts',(13.476865875366,-0.584737881352888,4.09880555174689));
#37024=CARTESIAN_POINT('Ctrl Pts',(13.5004799915159,-0.561568254327815,
3.80941662539381));
#37025=CARTESIAN_POINT('Ctrl Pts',(13.5240941076658,-0.403814885886516,
3.56570233148043));
#37026=CARTESIAN_POINT('Ctrl Pts',(13.5477082238157,-0.149284468950505,
3.42607049712074));
#37027=CARTESIAN_POINT('Ctrl Pts',(13.5713223399655,0.141023010189178,3.42398486344345));
#37028=CARTESIAN_POINT('Ctrl Pts',(13.5949364561154,0.39753334322815,3.55994526707815));
#37029=CARTESIAN_POINT('Ctrl Pts',(13.6185505722652,0.55877204319843,3.8013678508274));
#37030=CARTESIAN_POINT('Ctrl Pts',(13.6421646884151,0.586097133215014,4.09039401187145));
#37031=CARTESIAN_POINT('Ctrl Pts',(13.665778804565,0.47295996523623,4.35775661870721));
#37032=CARTESIAN_POINT('Ctrl Pts',(13.6893929207148,0.24647464915429,4.53938036140496));
#37033=CARTESIAN_POINT('Ctrl Pts',(13.7130070368647,-0.0390800323908759,
4.59173784568287));
#37034=CARTESIAN_POINT('Ctrl Pts',(13.7366211530146,-0.315268912124245,
4.50228123595558));
#37035=CARTESIAN_POINT('Ctrl Pts',(13.7602352691644,-0.515901402373503,
4.29244943148197));
#37036=CARTESIAN_POINT('Ctrl Pts',(13.7838493853143,-0.59289453017979,4.01253008491428));
#37037=CARTESIAN_POINT('Ctrl Pts',(13.8074635014642,-0.527796356489121,
3.72960781627073));
#37038=CARTESIAN_POINT('Ctrl Pts',(13.831077617614,-0.336208111796874,3.51148691674935));
#37039=CARTESIAN_POINT('Ctrl Pts',(13.8546917337639,-0.0640452526541193,
3.4104415783338));
#37040=CARTESIAN_POINT('Ctrl Pts',(13.8783058499138,0.223466497127862,3.45068801978614));
#37041=CARTESIAN_POINT('Ctrl Pts',(13.9019199660636,0.457422945247278,3.62258090124322));
#37042=CARTESIAN_POINT('Ctrl Pts',(13.9255340822135,0.581754800262342,3.88492489705937));
#37043=CARTESIAN_POINT('Ctrl Pts',(13.9491481983634,0.566665067602596,4.17484744237197));
#37044=CARTESIAN_POINT('Ctrl Pts',(13.9727623145132,0.415770106744681,4.42286658094793));
#37045=CARTESIAN_POINT('Ctrl Pts',(13.9963764306631,0.165232945489059,4.56954279968241));
#37046=CARTESIAN_POINT('Ctrl Pts',(14.019990546813,-0.124903441395439,4.57972412169294));
#37047=CARTESIAN_POINT('Ctrl Pts',(14.0436046629628,-0.385105849054417,
4.45097052228405));
#37048=CARTESIAN_POINT('Ctrl Pts',(14.0672187791127,-0.553014959135429,
4.21413869785145));
#37049=CARTESIAN_POINT('Ctrl Pts',(14.0908328952626,-0.58839018453545,3.92598704378684));
#37050=CARTESIAN_POINT('Ctrl Pts',(14.1144470114124,-0.482753606228458,
3.65557310990793));
#37051=CARTESIAN_POINT('Ctrl Pts',(14.1380611275623,-0.261421765577673,
3.46770347791168));
#37052=CARTESIAN_POINT('Ctrl Pts',(14.1616752437122,0.0225616210391343,
3.40740241293002));
#37053=CARTESIAN_POINT('Ctrl Pts',(14.185289359862,0.301137958114838,3.48912148496193));
#37054=CARTESIAN_POINT('Ctrl Pts',(14.2089034760119,0.507544487205137,3.69327614952086));
#37055=CARTESIAN_POINT('Ctrl Pts',(14.2325175921618,0.592314446747875,3.97093932005559));
#37056=CARTESIAN_POINT('Ctrl Pts',(14.2561317083116,0.535132125826274,4.25556708484021));
#37057=CARTESIAN_POINT('Ctrl Pts',(14.2797458244615,0.349701665714674,4.47894641865396));
#37058=CARTESIAN_POINT('Ctrl Pts',(14.3033599406114,0.0804627670229728,
4.58754290912926));
#37059=CARTESIAN_POINT('Ctrl Pts',(14.3269740567612,-0.208059593914322,
4.55533065134682));
#37060=CARTESIAN_POINT('Ctrl Pts',(14.3505881729111,-0.44671902479684,4.39002953712461));
#37061=CARTESIAN_POINT('Ctrl Pts',(14.374202289061,-0.578319131624566,4.13125512920294));
#37062=CARTESIAN_POINT('Ctrl Pts',(14.3978164052108,-0.571321032683373,
3.84102451585645));
#37063=CARTESIAN_POINT('Ctrl Pts',(14.4214305213607,-0.427401871100662,
3.58889348396707));
#37064=CARTESIAN_POINT('Ctrl Pts',(14.4450446375106,-0.181052875819672,
3.43528699049651));
#37065=CARTESIAN_POINT('Ctrl Pts',(14.4686587536604,0.108686701521778,3.41701790091169));
#37066=CARTESIAN_POINT('Ctrl Pts',(14.4922728698103,0.372378754238714,3.53846452970905));
#37067=CARTESIAN_POINT('Ctrl Pts',(14.5158869859602,0.546827646247725,3.77052134686598));
#37068=CARTESIAN_POINT('Ctrl Pts',(14.53950110211,0.59022548618159,4.05757432072539));
#37069=CARTESIAN_POINT('Ctrl Pts',(14.5631152182599,0.492171679592087,4.3308292078278));
#37070=CARTESIAN_POINT('Ctrl Pts',(14.5867293344098,0.276165503816305,4.52479857226205));
#37071=CARTESIAN_POINT('Ctrl Pts',(14.6103434505596,-0.00602565743375084,
4.59299630554951));
#37072=CARTESIAN_POINT('Ctrl Pts',(14.6339575667095,-0.286772727926288,
4.51907834617235));
#37073=CARTESIAN_POINT('Ctrl Pts',(14.6575716828594,-0.49879271786407,4.32075964763751));
#37074=CARTESIAN_POINT('Ctrl Pts',(14.6811857990092,-0.591273560669336,
4.04556866666751));
#37075=CARTESIAN_POINT('Ctrl Pts',(14.7047999151591,-0.542051578672567,
3.75945683743125));
#37076=CARTESIAN_POINT('Ctrl Pts',(14.728414031309,-0.362923162297683,3.53099285177933));
#37077=CARTESIAN_POINT('Ctrl Pts',(14.7520281474588,-0.0968176839575538,
3.41492969374656));
#37078=CARTESIAN_POINT('Ctrl Pts',(14.7756422636087,0.192490826988301,3.43908270827084));
#37079=CARTESIAN_POINT('Ctrl Pts',(14.7992563797586,0.435667569828913,3.59766345479839));
#37080=CARTESIAN_POINT('Ctrl Pts',(14.8228704959084,0.574433549780463,3.85266695881428));
#37081=CARTESIAN_POINT('Ctrl Pts',(14.8464846120583,0.575532524168,4.14297984400973));
#37082=CARTESIAN_POINT('Ctrl Pts',(14.8700987282082,0.438701136655627,4.39902663091346));
#37083=CARTESIAN_POINT('Ctrl Pts',(14.893712844358,0.196731937819222,4.55944387228049));
#37084=CARTESIAN_POINT('Ctrl Pts',(14.9173269605079,-0.0923853752310475,
4.58578657160514));
#37085=CARTESIAN_POINT('Ctrl Pts',(14.9409410766578,-0.359362027571537,
4.47174127747511));
#37086=CARTESIAN_POINT('Ctrl Pts',(14.9645551928076,-0.540214773976066,
4.24464025294543));
#37087=CARTESIAN_POINT('Ctrl Pts',(14.9881693089575,-0.59160192159185,3.95890873763601));
#37088=CARTESIAN_POINT('Ctrl Pts',(15.0117834251074,-0.501206205285789,
3.68302663884805));
#37089=CARTESIAN_POINT('Ctrl Pts',(15.0353975412572,-0.290695865081771,
3.48310596742652));
#37090=CARTESIAN_POINT('Ctrl Pts',(15.0590116574071,-0.0105122258222001,
3.40706994202017));
#37091=CARTESIAN_POINT('Ctrl Pts',(15.082625773557,0.272176412698783,3.47311795657709));
#37092=CARTESIAN_POINT('Ctrl Pts',(15.1062398897068,0.489659512974156,3.66547122397039));
#37093=CARTESIAN_POINT('Ctrl Pts',(15.1219826338067,0.5563490739778,3.84710486709154));
#37094=CARTESIAN_POINT('Ctrl Pts',(15.1298540058567,0.566167676482186,3.94044192881839));
#37095=CARTESIAN_POINT('Ctrl Pts',(12.4701459941433,0.254789069842909,4.44592641788345));
#37096=CARTESIAN_POINT('Ctrl Pts',(12.4780173661933,0.181274697121691,4.48793034026739));
#37097=CARTESIAN_POINT('Ctrl Pts',(12.4937601102932,0.0131377437512366,
4.53483083224977));
#37098=CARTESIAN_POINT('Ctrl Pts',(12.517374226443,-0.242323003376296,4.47697306011837));
#37099=CARTESIAN_POINT('Ctrl Pts',(12.5409883425929,-0.439671888977142,
4.30480445207012));
#37100=CARTESIAN_POINT('Ctrl Pts',(12.5646024587428,-0.531669448515955,
4.05958515863483));
#37101=CARTESIAN_POINT('Ctrl Pts',(12.5882165748926,-0.496240142441994,
3.80008637217214));
#37102=CARTESIAN_POINT('Ctrl Pts',(12.6118306910425,-0.341887499674706,
3.58849794711368));
#37103=CARTESIAN_POINT('Ctrl Pts',(12.6354448071924,-0.105597250297878,
3.47552899021694));
#37104=CARTESIAN_POINT('Ctrl Pts',(12.6590589233422,0.155999231932725,3.4882530946792));
#37105=CARTESIAN_POINT('Ctrl Pts',(12.6826730394921,0.380209824197002,3.62362093815591));
#37106=CARTESIAN_POINT('Ctrl Pts',(12.706287155642,0.513300292941022,3.84919062944795));
#37107=CARTESIAN_POINT('Ctrl Pts',(12.7299012717918,0.52337486302099,4.11090284295443));
#37108=CARTESIAN_POINT('Ctrl Pts',(12.7535153879417,0.408018961865605,4.34603641497018));
#37109=CARTESIAN_POINT('Ctrl Pts',(12.7771295040916,0.194878495711741,4.49823995272895));
#37110=CARTESIAN_POINT('Ctrl Pts',(12.8007436202414,-0.0649659676909401,
4.53103681671432));
#37111=CARTESIAN_POINT('Ctrl Pts',(12.8243577363913,-0.30924088042124,4.43656701116699));
#37112=CARTESIAN_POINT('Ctrl Pts',(12.8479718525412,-0.479404065419363,
4.23747088215356));
#37113=CARTESIAN_POINT('Ctrl Pts',(12.871585968691,-0.534674727916345,3.9814632031866));
#37114=CARTESIAN_POINT('Ctrl Pts',(12.8952000848409,-0.461806870250484,
3.72989799658434));
#37115=CARTESIAN_POINT('Ctrl Pts',(12.9188142009908,-0.278263781132688,
3.54306461538724));
#37116=CARTESIAN_POINT('Ctrl Pts',(12.9424283171406,-0.0280328398727138,
3.46573897998727));
#37117=CARTESIAN_POINT('Ctrl Pts',(12.9660424332905,0.228916366652986,3.51645271720832));
#37118=CARTESIAN_POINT('Ctrl Pts',(12.9896565494404,0.431004172325429,3.68305192688505));
#37119=CARTESIAN_POINT('Ctrl Pts',(13.0132706655902,0.529798827743877,3.92560994866724));
#37120=CARTESIAN_POINT('Ctrl Pts',(13.0368847817401,0.501623505980173,4.1859960641053));
#37121=CARTESIAN_POINT('Ctrl Pts',(13.06049889789,0.353230619039521,4.40180692799916));
#37122=CARTESIAN_POINT('Ctrl Pts',(13.0841130140398,0.120183555287252,4.52132196448402));
#37123=CARTESIAN_POINT('Ctrl Pts',(13.1077271301897,-0.14166633412753,4.51589856308179));
#37124=CARTESIAN_POINT('Ctrl Pts',(13.1313412463396,-0.369564900381594,
4.38683647969259));
#37125=CARTESIAN_POINT('Ctrl Pts',(13.1549553624894,-0.508894665592834,
4.16506634104549));
#37126=CARTESIAN_POINT('Ctrl Pts',(13.1785694786393,-0.5262642816069,3.9037369046842));
#37127=CARTESIAN_POINT('Ctrl Pts',(13.2021835947892,-0.417510999030181,
3.66547758923531));
#37128=CARTESIAN_POINT('Ctrl Pts',(13.225797710939,-0.208698299100604,3.50738889824983));
#37129=CARTESIAN_POINT('Ctrl Pts',(13.2494118270889,0.0501304010278875,
3.46735788703128));
#37130=CARTESIAN_POINT('Ctrl Pts',(13.2730259432388,0.296945001575366,3.55497826608759));
#37131=CARTESIAN_POINT('Ctrl Pts',(13.2966400593886,0.472594665360713,3.74925120162283));
#37132=CARTESIAN_POINT('Ctrl Pts',(13.3202541755385,0.534983727701048,4.00361783223636));
#37133=CARTESIAN_POINT('Ctrl Pts',(13.3438682916884,0.469160215495142,4.25711742416948));
#37134=CARTESIAN_POINT('Ctrl Pts',(13.3674824078382,0.290899191662876,4.44899703551904));
#37135=CARTESIAN_POINT('Ctrl Pts',(13.3910965239881,0.0429221515009326,
4.53327138168622));
#37136=CARTESIAN_POINT('Ctrl Pts',(13.414710640138,-0.215341481063824,4.48974352894983));
#37137=CARTESIAN_POINT('Ctrl Pts',(13.4383247562878,-0.421997028626747,
4.32884523023027));
#37138=CARTESIAN_POINT('Ctrl Pts',(13.4619388724377,-0.527518050615216,
4.08913688288313));
#37139=CARTESIAN_POINT('Ctrl Pts',(13.4855529885876,-0.506615699542168,
3.82806626104107));
#37140=CARTESIAN_POINT('Ctrl Pts',(13.5091671047374,-0.364299369350597,
3.60820075662942));
#37141=CARTESIAN_POINT('Ctrl Pts',(13.5327812208873,-0.134676159283021,
3.48223266833859));
#37142=CARTESIAN_POINT('Ctrl Pts',(13.5563953370372,0.127223129883027,3.48035112543394));
#37143=CARTESIAN_POINT('Ctrl Pts',(13.580009453187,0.35863251032937,3.60300705277064));
#37144=CARTESIAN_POINT('Ctrl Pts',(13.6036235693369,0.504093113113068,3.82080510351303));
#37145=CARTESIAN_POINT('Ctrl Pts',(13.6272376854868,0.528744292176554,4.08154845863482));
#37146=CARTESIAN_POINT('Ctrl Pts',(13.6508518016366,0.426678220852065,4.32274815795836));
#37147=CARTESIAN_POINT('Ctrl Pts',(13.6744659177865,0.222355743648963,4.48659901446809));
#37148=CARTESIAN_POINT('Ctrl Pts',(13.6980800339364,-0.0352558354131549,
4.53383302978021));
#37149=CARTESIAN_POINT('Ctrl Pts',(13.7216941500862,-0.284418108090716,
4.45313024331322));
#37150=CARTESIAN_POINT('Ctrl Pts',(13.7453082662361,-0.465417601233682,
4.26383163964332));
#37151=CARTESIAN_POINT('Ctrl Pts',(13.768922382386,-0.534876526311652,4.01130394691162));
#37152=CARTESIAN_POINT('Ctrl Pts',(13.7925364985358,-0.476148568402614,
3.75606718461195));
#37153=CARTESIAN_POINT('Ctrl Pts',(13.8161506146857,-0.303308291444651,
3.55929061961886));
#37154=CARTESIAN_POINT('Ctrl Pts',(13.8397647308356,-0.0577780710103693,
3.46813312556118));
#37155=CARTESIAN_POINT('Ctrl Pts',(13.8633788469854,0.201599066354243,3.50444123046797));
#37156=CARTESIAN_POINT('Ctrl Pts',(13.8869929631353,0.412661584067771,3.65951344424533));
#37157=CARTESIAN_POINT('Ctrl Pts',(13.9106070792852,0.52482688048259,3.89618563135138));
#37158=CARTESIAN_POINT('Ctrl Pts',(13.934221195435,0.511213761492322,4.157737654591));
#37159=CARTESIAN_POINT('Ctrl Pts',(13.9578353115849,0.375084705828511,4.38148675084272));
#37160=CARTESIAN_POINT('Ctrl Pts',(13.9814494277348,0.149063989321389,4.51380989159668));
#37161=CARTESIAN_POINT('Ctrl Pts',(14.0050635438846,-0.112680949911453,
4.52299491502504));
#37162=CARTESIAN_POINT('Ctrl Pts',(14.0286776600345,-0.347421115087809,
4.40684056632315));
#37163=CARTESIAN_POINT('Ctrl Pts',(14.0522917761844,-0.498899391517477,
4.19318404374712));
#37164=CARTESIAN_POINT('Ctrl Pts',(14.0759058923342,-0.530812955762567,
3.93322962026762));
#37165=CARTESIAN_POINT('Ctrl Pts',(14.0995200084841,-0.435513499990629,
3.68927718310219));
#37166=CARTESIAN_POINT('Ctrl Pts',(14.123134124634,-0.235840202189154,3.51979163205294));
#37167=CARTESIAN_POINT('Ctrl Pts',(14.1467482407838,0.020353841830372,3.46539135927508));
#37168=CARTESIAN_POINT('Ctrl Pts',(14.1703623569337,0.271669945965271,3.53911376883853));
#37169=CARTESIAN_POINT('Ctrl Pts',(14.1939764730836,0.457878456363209,3.72329077208477));
#37170=CARTESIAN_POINT('Ctrl Pts',(14.2175905892334,0.534353207246894,3.97378306806742));
#37171=CARTESIAN_POINT('Ctrl Pts',(14.2412047053833,0.482766492200443,4.23055843429265));
#37172=CARTESIAN_POINT('Ctrl Pts',(14.2648188215332,0.315481426597312,4.4320788667444));
#37173=CARTESIAN_POINT('Ctrl Pts',(14.288432937683,0.0725890409372144,4.53004859093371));
#37174=CARTESIAN_POINT('Ctrl Pts',(14.3120470538329,-0.187699813700353,
4.50098848045824));
#37175=CARTESIAN_POINT('Ctrl Pts',(14.3356611699828,-0.40300510134274,4.35186299309067));
#37176=CARTESIAN_POINT('Ctrl Pts',(14.3592752861326,-0.521727410993515,
4.11841108999162));
#37177=CARTESIAN_POINT('Ctrl Pts',(14.3828894022825,-0.515414114678713,
3.85658114487643));
#37178=CARTESIAN_POINT('Ctrl Pts',(14.4065035184324,-0.385578237809175,
3.62912252677875));
#37179=CARTESIAN_POINT('Ctrl Pts',(14.4301176345822,-0.163335852108122,
3.49054727694211));
#37180=CARTESIAN_POINT('Ctrl Pts',(14.4537317507321,0.0980511075867261,
3.47406591865897));
#37181=CARTESIAN_POINT('Ctrl Pts',(14.477345866882,0.335939436781555,3.58362832417432));
#37182=CARTESIAN_POINT('Ctrl Pts',(14.5009599830318,0.493317541363497,3.79297710030521));
#37183=CARTESIAN_POINT('Ctrl Pts',(14.5245740991817,0.532468663007706,4.05194035550473));
#37184=CARTESIAN_POINT('Ctrl Pts',(14.5481882153316,0.444009962867018,4.2984557429324));
#37185=CARTESIAN_POINT('Ctrl Pts',(14.5718023314814,0.249141184223067,4.47344413391656));
#37186=CARTESIAN_POINT('Ctrl Pts',(14.5954164476313,-0.00543601357889273,
4.53496834239941));
#37187=CARTESIAN_POINT('Ctrl Pts',(14.6190305637812,-0.258710432878536,
4.46828366353805));
#37188=CARTESIAN_POINT('Ctrl Pts',(14.642644679931,-0.449983095981302,4.28937154481299));
#37189=CARTESIAN_POINT('Ctrl Pts',(14.6662587960809,-0.533414177619135,
4.0411095209942));
#37190=CARTESIAN_POINT('Ctrl Pts',(14.6898729122308,-0.489008838375032,
3.78299531421925));
#37191=CARTESIAN_POINT('Ctrl Pts',(14.7134870283806,-0.327409126727749,
3.57688779119022));
#37192=CARTESIAN_POINT('Ctrl Pts',(14.7371011445305,-0.0873435389344073,
3.47218205409647));
#37193=CARTESIAN_POINT('Ctrl Pts',(14.7607152606804,0.173654536592096,3.49397156277145));
#37194=CARTESIAN_POINT('Ctrl Pts',(14.7843293768302,0.393035092271916,3.63703430753458));
#37195=CARTESIAN_POINT('Ctrl Pts',(14.8079434929801,0.518222054789869,3.86708431049878));
#37196=CARTESIAN_POINT('Ctrl Pts',(14.8315576091299,0.519213488464815,4.12898847670818));
#37197=CARTESIAN_POINT('Ctrl Pts',(14.8551717252798,0.395771807832633,4.35997967156842));
#37198=CARTESIAN_POINT('Ctrl Pts',(14.8787858414297,0.177480631307892,4.50469920000947));
#37199=CARTESIAN_POINT('Ctrl Pts',(14.9023999575796,-0.0833449560929437,
4.52846412073519));
#37200=CARTESIAN_POINT('Ctrl Pts',(14.9260140737294,-0.324196468699902,
4.42557878841823));
#37201=CARTESIAN_POINT('Ctrl Pts',(14.9496281898793,-0.487351775161311,
4.22070085323907));
#37202=CARTESIAN_POINT('Ctrl Pts',(14.9732423060292,-0.533710406612102,
3.96292974457304));
#37203=CARTESIAN_POINT('Ctrl Pts',(14.996856422179,-0.452160410331013,3.71404423263127));
#37204=CARTESIAN_POINT('Ctrl Pts',(15.0204705383289,-0.262249669398955,
3.53368690291293));
#37205=CARTESIAN_POINT('Ctrl Pts',(15.0440846544788,-0.0094835464747447,
3.46509142247974));
#37206=CARTESIAN_POINT('Ctrl Pts',(15.0676987706286,0.245542447700007,3.52467627408104));
#37207=CARTESIAN_POINT('Ctrl Pts',(15.0913128867785,0.441743625625371,3.69820671204414));
#37208=CARTESIAN_POINT('Ctrl Pts',(15.1070556308784,0.501907244810829,3.86206650016617));
#37209=CARTESIAN_POINT('Ctrl Pts',(15.1149270029284,0.510765042839744,3.94627001497588));
#37210=CARTESIAN_POINT('Ctrl Pts',(12.4552189912149,0.227152124655503,4.39755682347243));
#37211=CARTESIAN_POINT('Ctrl Pts',(12.4630903632649,0.161611848667067,4.43500458455284));
#37212=CARTESIAN_POINT('Ctrl Pts',(12.4788331073648,0.0117126939868845,
4.476817784812));
#37213=CARTESIAN_POINT('Ctrl Pts',(12.5024472235147,-0.216038251184659,
4.42523583949706));
#37214=CARTESIAN_POINT('Ctrl Pts',(12.5260613396645,-0.391980722697534,
4.27174234332294));
#37215=CARTESIAN_POINT('Ctrl Pts',(12.5496754558144,-0.473999316058885,
4.05312196237532));
#37216=CARTESIAN_POINT('Ctrl Pts',(12.5732895719643,-0.442413023308054,
3.82177098359562));
#37217=CARTESIAN_POINT('Ctrl Pts',(12.5969036881141,-0.304802996424253,
3.6331335340607));
#37218=CARTESIAN_POINT('Ctrl Pts',(12.620517804264,-0.0941431270098475,
3.53241830873714));
#37219=CARTESIAN_POINT('Ctrl Pts',(12.6441319204139,0.139078010685439,3.54376223084778));
#37220=CARTESIAN_POINT('Ctrl Pts',(12.6677460365637,0.338968502198674,3.66444673774097));
#37221=CARTESIAN_POINT('Ctrl Pts',(12.6913601527136,0.457622660971028,3.86554890694496));
#37222=CARTESIAN_POINT('Ctrl Pts',(12.7149742688635,0.46660444343158,4.09887322255608));
#37223=CARTESIAN_POINT('Ctrl Pts',(12.7385883850133,0.36376118545685,4.30850187928827));
#37224=CARTESIAN_POINT('Ctrl Pts',(12.7622025011632,0.173740044570527,4.44419591437112));
#37225=CARTESIAN_POINT('Ctrl Pts',(12.7858166173131,-0.0579191156056905,
4.47343530576616));
#37226=CARTESIAN_POINT('Ctrl Pts',(12.809430733463,-0.275697552729921,4.38921263067613));
#37227=CARTESIAN_POINT('Ctrl Pts',(12.8330448496128,-0.42740315389367,4.2117124390707));
#37228=CARTESIAN_POINT('Ctrl Pts',(12.8566589657627,-0.476678613100171,
3.98347388770222));
#37229=CARTESIAN_POINT('Ctrl Pts',(12.8802730819125,-0.411714724743029,
3.75919593416074));
#37230=CARTESIAN_POINT('Ctrl Pts',(12.9038871980624,-0.248080536335154,
3.59262835132974));
#37231=CARTESIAN_POINT('Ctrl Pts',(12.9275013142123,-0.0249921205063485,
3.52369021994808));
#37232=CARTESIAN_POINT('Ctrl Pts',(12.9511154303621,0.204085831019768,3.5689030431123));
#37233=CARTESIAN_POINT('Ctrl Pts',(12.974729546512,0.384253192413122,3.71743125300502));
#37234=CARTESIAN_POINT('Ctrl Pts',(12.9983436626619,0.472331601336806,3.93367903017235));
#37235=CARTESIAN_POINT('Ctrl Pts',(13.0219577788117,0.44721245393608,4.16582108944128));
#37236=CARTESIAN_POINT('Ctrl Pts',(13.0455718949616,0.314915728754283,4.35822297028905));
#37237=CARTESIAN_POINT('Ctrl Pts',(13.0691860111115,0.107147256940744,4.46477422259573));
#37238=CARTESIAN_POINT('Ctrl Pts',(13.0928001272613,-0.126299800886535,
4.4599390970068));
#37239=CARTESIAN_POINT('Ctrl Pts',(13.1164142434112,-0.329478232215912,
4.34487636502855));
#37240=CARTESIAN_POINT('Ctrl Pts',(13.1400283595611,-0.453694911585238,
4.14716161137019));
#37241=CARTESIAN_POINT('Ctrl Pts',(13.1636424757109,-0.469180447069464,
3.9141785531052));
#37242=CARTESIAN_POINT('Ctrl Pts',(13.1872565918608,-0.372223622289685,
3.70176320202068));
#37243=CARTESIAN_POINT('Ctrl Pts',(13.2108707080107,-0.186060815253654,
3.56082237569912));
#37244=CARTESIAN_POINT('Ctrl Pts',(13.2344848241605,0.0446927613901878,
3.52513352430527));
#37245=CARTESIAN_POINT('Ctrl Pts',(13.2580989403104,0.26473540664544,3.60324972951781));
#37246=CARTESIAN_POINT('Ctrl Pts',(13.2817130564603,0.421332368785403,3.77644989896424));
#37247=CARTESIAN_POINT('Ctrl Pts',(13.3053271726101,0.476954095708811,4.00322540633176));
#37248=CARTESIAN_POINT('Ctrl Pts',(13.32894128876,0.418270453356816,4.22922792261873));
#37249=CARTESIAN_POINT('Ctrl Pts',(13.3525554049099,0.259345385135757,4.40029437151701));
#37250=CARTESIAN_POINT('Ctrl Pts',(13.3761695210597,0.0382663899759653,
4.47542748769673));
#37251=CARTESIAN_POINT('Ctrl Pts',(13.3997836372096,-0.19198341192685,4.43662109683837));
#37252=CARTESIAN_POINT('Ctrl Pts',(13.4233977533595,-0.376223052699929,
4.29317542065556));
#37253=CARTESIAN_POINT('Ctrl Pts',(13.4470118695093,-0.470298219877544,
4.07946821401937));
#37254=CARTESIAN_POINT('Ctrl Pts',(13.4706259856592,-0.451663144756522,
3.84671589668833));
#37255=CARTESIAN_POINT('Ctrl Pts',(13.4942401018091,-0.324783852814677,
3.65069918177841));
#37256=CARTESIAN_POINT('Ctrl Pts',(13.5178542179589,-0.120067849615538,
3.53839483955645));
#37257=CARTESIAN_POINT('Ctrl Pts',(13.5414683341088,0.113423249576877,3.53671738742444));
#37258=CARTESIAN_POINT('Ctrl Pts',(13.5650824502587,0.319731677430589,3.64606883846313));
#37259=CARTESIAN_POINT('Ctrl Pts',(13.5886965664085,0.449414183027706,3.84024235619866));
#37260=CARTESIAN_POINT('Ctrl Pts',(13.6123106825584,0.471391451138094,4.07270290539818));
#37261=CARTESIAN_POINT('Ctrl Pts',(13.6359247987083,0.380396476467901,4.28773969720951));
#37262=CARTESIAN_POINT('Ctrl Pts',(13.6595389148581,0.198236838143636,4.43381766753122));
#37263=CARTESIAN_POINT('Ctrl Pts',(13.683153031008,-0.0314316384354341,
4.47592821387755));
#37264=CARTESIAN_POINT('Ctrl Pts',(13.7067671471579,-0.253567304057185,
4.40397925067086));
#37265=CARTESIAN_POINT('Ctrl Pts',(13.7303812633077,-0.414933800093862,
4.23521384780468));
#37266=CARTESIAN_POINT('Ctrl Pts',(13.7539953794576,-0.476858522443512,
4.01007780890896));
#37267=CARTESIAN_POINT('Ctrl Pts',(13.7776094956075,-0.424500780316106,
3.78252655295316));
#37268=CARTESIAN_POINT('Ctrl Pts',(13.8012236117573,-0.270408471092428,
3.60709432248837));
#37269=CARTESIAN_POINT('Ctrl Pts',(13.8248377279072,-0.0515108893666192,
3.52582467278856));
#37270=CARTESIAN_POINT('Ctrl Pts',(13.8484518440571,0.179731635580624,3.55819444114981));
#37271=CARTESIAN_POINT('Ctrl Pts',(13.8720659602069,0.367900222888263,3.69644598724744));
#37272=CARTESIAN_POINT('Ctrl Pts',(13.8956800763568,0.467898960702838,3.90744636564338));
#37273=CARTESIAN_POINT('Ctrl Pts',(13.9192941925067,0.455762455382048,4.14062786681004));
#37274=CARTESIAN_POINT('Ctrl Pts',(13.9429083086565,0.33439930491234,4.34010692073752));
#37275=CARTESIAN_POINT('Ctrl Pts',(13.9665224248064,0.132895033153719,4.45807698351094));
#37276=CARTESIAN_POINT('Ctrl Pts',(13.9901365409563,-0.100458458427467,
4.46626570835715));
#37277=CARTESIAN_POINT('Ctrl Pts',(14.0137506571061,-0.309736381121202,
4.36271061036225));
#37278=CARTESIAN_POINT('Ctrl Pts',(14.037364773256,-0.444783823899526,4.1722293896428));
#37279=CARTESIAN_POINT('Ctrl Pts',(14.0609788894059,-0.473235726989685,
3.94047219674841));
#37280=CARTESIAN_POINT('Ctrl Pts',(14.0845930055557,-0.388273393752801,
3.72298125629644));
#37281=CARTESIAN_POINT('Ctrl Pts',(14.1082071217056,-0.210258638800633,
3.5718797861942));
#37282=CARTESIAN_POINT('Ctrl Pts',(14.1318212378555,0.0181460626216094,
3.52338030562014));
#37283=CARTESIAN_POINT('Ctrl Pts',(14.1554353540053,0.242201933815703,3.58910605271512));
#37284=CARTESIAN_POINT('Ctrl Pts',(14.1790494701552,0.40821242552128,3.75330539464867));
#37285=CARTESIAN_POINT('Ctrl Pts',(14.2026635863051,0.476391967745912,3.97662681607925));
#37286=CARTESIAN_POINT('Ctrl Pts',(14.2262777024549,0.430400858574612,4.20554978374509));
#37287=CARTESIAN_POINT('Ctrl Pts',(14.2498918186048,0.28126118747995,4.38521131483484));
#37288=CARTESIAN_POINT('Ctrl Pts',(14.2735059347547,0.0647153148514563,
4.47255427273816));
#37289=CARTESIAN_POINT('Ctrl Pts',(14.2971200509045,-0.167340033486385,
4.44664630956965));
#37290=CARTESIAN_POINT('Ctrl Pts',(14.3207341670544,-0.359291177888639,
4.31369644905674));
#37291=CARTESIAN_POINT('Ctrl Pts',(14.3443482832043,-0.465135690362464,
4.10556705078029));
#37292=CARTESIAN_POINT('Ctrl Pts',(14.3679623993541,-0.459507196674052,
3.87213777389641));
#37293=CARTESIAN_POINT('Ctrl Pts',(14.391576515504,-0.343754604517688,3.66935156959044));
#37294=CARTESIAN_POINT('Ctrl Pts',(14.4151906316539,-0.145618828396573,
3.5458075633877));
#37295=CARTESIAN_POINT('Ctrl Pts',(14.4388047478037,0.0874155136516737,
3.53111393640625));
#37296=CARTESIAN_POINT('Ctrl Pts',(14.4624188639536,0.299500119324396,3.6287921186396));
#37297=CARTESIAN_POINT('Ctrl Pts',(14.4860329801035,0.439807436479269,3.81543285374444));
#37298=CARTESIAN_POINT('Ctrl Pts',(14.5096470962533,0.474711839833821,4.04630639028407));
#37299=CARTESIAN_POINT('Ctrl Pts',(14.5332612124032,0.395848246141948,4.26608227803701));
#37300=CARTESIAN_POINT('Ctrl Pts',(14.5568753285531,0.22211686462983,4.42208969557108));
#37301=CARTESIAN_POINT('Ctrl Pts',(14.5804894447029,-0.00484636972403486,
4.47694037924932));
#37302=CARTESIAN_POINT('Ctrl Pts',(14.6041035608528,-0.230648137830783,
4.41748898090375));
#37303=CARTESIAN_POINT('Ctrl Pts',(14.6277176770027,-0.401173474098533,
4.25798344198848));
#37304=CARTESIAN_POINT('Ctrl Pts',(14.6513317931525,-0.475554794568933,
4.03665037532088));
#37305=CARTESIAN_POINT('Ctrl Pts',(14.6749459093024,-0.435966098077497,
3.80653379100725));
#37306=CARTESIAN_POINT('Ctrl Pts',(14.6985600254523,-0.291895091157815,
3.62278273060111));
#37307=CARTESIAN_POINT('Ctrl Pts',(14.7221741416021,-0.077869393911261,
3.52943441444639));
#37308=CARTESIAN_POINT('Ctrl Pts',(14.745788257752,0.15481824619589,3.54886041727207));
#37309=CARTESIAN_POINT('Ctrl Pts',(14.7694023739019,0.350402614714918,3.67640516027076));
#37310=CARTESIAN_POINT('Ctrl Pts',(14.7930164900517,0.462010559799276,3.88150166218328));
#37311=CARTESIAN_POINT('Ctrl Pts',(14.8166306062016,0.46289445276163,4.11499710940664));
#37312=CARTESIAN_POINT('Ctrl Pts',(14.8402447223515,0.352842479009638,4.32093271222338));
#37313=CARTESIAN_POINT('Ctrl Pts',(14.8638588385013,0.158229324796562,4.44995452773844));
#37314=CARTESIAN_POINT('Ctrl Pts',(14.8874729546512,-0.07430453695484,4.47114166986524));
#37315=CARTESIAN_POINT('Ctrl Pts',(14.9110870708011,-0.289030909828268,
4.37941629936134));
#37316=CARTESIAN_POINT('Ctrl Pts',(14.9347011869509,-0.434488776346555,
4.1967614535327));
#37317=CARTESIAN_POINT('Ctrl Pts',(14.9583153031008,-0.475818891632353,
3.96695075151007));
#37318=CARTESIAN_POINT('Ctrl Pts',(14.9819294192507,-0.403114615376237,
3.74506182641449));
#37319=CARTESIAN_POINT('Ctrl Pts',(15.0055435354005,-0.233803473716137,
3.58426783839933));
#37320=CARTESIAN_POINT('Ctrl Pts',(15.0291576515504,-0.00845486712728951,
3.5231129029393));
#37321=CARTESIAN_POINT('Ctrl Pts',(15.0527717677003,0.218908482701231,3.57623459158499));
#37322=CARTESIAN_POINT('Ctrl Pts',(15.0763858838501,0.393827738276586,3.73094220011788));
#37323=CARTESIAN_POINT('Ctrl Pts',(15.09212862795,0.447465415643859,3.87702813324079));
#37324=CARTESIAN_POINT('Ctrl Pts',(15.1,0.455362409197302,3.95209810113337));
#37325=CARTESIAN_POINT('',(15.1,0.455362409197302,3.95209810113338));
#37326=CARTESIAN_POINT('Ctrl Pts',(15.1,0.455362409197302,3.95209810113337));
#37327=CARTESIAN_POINT('Ctrl Pts',(15.1,0.461198486074795,3.93070554260298));
#37328=CARTESIAN_POINT('Ctrl Pts',(15.1,0.46535922191849,3.9089149747703));
#37329=CARTESIAN_POINT('Ctrl Pts',(15.1,0.467933495509747,3.88694781877637));
#37330=CARTESIAN_POINT('Ctrl Pts',(15.1,0.470556099470815,3.86456824322593));
#37331=CARTESIAN_POINT('Ctrl Pts',(15.1,0.471533159003394,3.84200460508655));
#37332=CARTESIAN_POINT('Ctrl Pts',(15.1,0.470938919222204,3.8194389967166));
#37333=CARTESIAN_POINT('Ctrl Pts',(15.1,0.470570970565677,3.80546654730098));
#37334=CARTESIAN_POINT('Ctrl Pts',(15.1,0.469600118414825,3.7914923521806));
#37335=CARTESIAN_POINT('Ctrl Pts',(15.1,0.468037922355437,3.77755218535593));
#37336=CARTESIAN_POINT('Ctrl Pts',(15.1,0.467305764617198,3.77101881782393));
#37337=CARTESIAN_POINT('Ctrl Pts',(15.1,0.466444065557791,3.76449770946228));
#37338=CARTESIAN_POINT('Ctrl Pts',(15.1,0.465455885979624,3.7580011302485));
#37339=CARTESIAN_POINT('Ctrl Pts',(15.1,0.462059294618766,3.73567095330476));
#37340=CARTESIAN_POINT('Ctrl Pts',(15.1,0.45716703427379,3.71360451488159));
#37341=CARTESIAN_POINT('Ctrl Pts',(15.1,0.450855318277529,3.69195899424001));
#37342=CARTESIAN_POINT('Ctrl Pts',(15.1,0.444011336009419,3.66848810937402));
#37343=CARTESIAN_POINT('Ctrl Pts',(15.1,0.435499564516811,3.64551127788848));
#37344=CARTESIAN_POINT('Ctrl Pts',(15.1,0.425460105602329,3.62314791088594));
#37345=CARTESIAN_POINT('Ctrl Pts',(15.1,0.421555366121865,3.61444992000866));
#37346=CARTESIAN_POINT('Ctrl Pts',(15.1,0.417417266816347,3.60584160863805));
#37347=CARTESIAN_POINT('Ctrl Pts',(15.1,0.413065612826793,3.5973533346642));
#37348=CARTESIAN_POINT('Ctrl Pts',(15.1,0.400188909388694,3.57223622128044));
#37349=CARTESIAN_POINT('Ctrl Pts',(15.1,0.385429835973237,3.54813135585314));
#37350=CARTESIAN_POINT('Ctrl Pts',(15.1,0.369010648251791,3.52520488756047));
#37351=CARTESIAN_POINT('Ctrl Pts',(15.1,0.352591460530346,3.50227841926781));
#37352=CARTESIAN_POINT('Ctrl Pts',(15.1,0.334512091502091,3.48052876229398));
#37353=CARTESIAN_POINT('Ctrl Pts',(15.1,0.31493781544227,3.46010549098216));
#37354=CARTESIAN_POINT('Ctrl Pts',(14.8800042915148,-1.01702808208336E-5,
4.45785711824254));
#37355=CARTESIAN_POINT('Ctrl Pts',(14.8824938458936,-0.0238866377941533,
4.45787702641871));
#37356=CARTESIAN_POINT('Ctrl Pts',(14.8849834002724,-0.0477600743578134,
4.45604121816599));
#37357=CARTESIAN_POINT('Ctrl Pts',(14.8874729546512,-0.0713366221418418,
4.45232291776013));
#37358=CARTESIAN_POINT('Ctrl Pts',(14.8953443267012,-0.145879994579315,
4.44056654636394));
#37359=CARTESIAN_POINT('Ctrl Pts',(14.9032156987511,-0.217455452203791,
4.40999142286264));
#37360=CARTESIAN_POINT('Ctrl Pts',(14.9110870708011,-0.277486158769077,
4.36426138680722));
#37361=CARTESIAN_POINT('Ctrl Pts',(14.918958442851,-0.337516865334364,4.31853135075179));
#37362=CARTESIAN_POINT('Ctrl Pts',(14.926829814901,-0.38600282084046,4.25764640214225));
#37363=CARTESIAN_POINT('Ctrl Pts',(14.9347011869509,-0.417134151141141,
4.18890214416703));
#37364=CARTESIAN_POINT('Ctrl Pts',(14.9425725590009,-0.448265481441821,
4.12015788619182));
#37365=CARTESIAN_POINT('Ctrl Pts',(14.9504439310508,-0.462042186537087,
4.04355431885095));
#37366=CARTESIAN_POINT('Ctrl Pts',(14.9583153031008,-0.456813159708701,
3.96827104766458));
#37367=CARTESIAN_POINT('Ctrl Pts',(14.9661866751508,-0.451584132880315,
3.89298777647821));
#37368=CARTESIAN_POINT('Ctrl Pts',(14.9740580472007,-0.427349374128277,
3.81902480144635));
#37369=CARTESIAN_POINT('Ctrl Pts',(14.9819294192507,-0.387013471142241,
3.7552443159279));
#37370=CARTESIAN_POINT('Ctrl Pts',(14.9898007913006,-0.346677568156205,
3.69146383040944));
#37371=CARTESIAN_POINT('Ctrl Pts',(14.9976721633506,-0.290240520936171,
3.63786583440439));
#37372=CARTESIAN_POINT('Ctrl Pts',(15.0055435354005,-0.224463896228013,
3.60087434715852));
#37373=CARTESIAN_POINT('Ctrl Pts',(15.0134149074505,-0.158687271519854,
3.56388285991266));
#37374=CARTESIAN_POINT('Ctrl Pts',(15.0212862795004,-0.0835710693235713,
3.54349788142598));
#37375=CARTESIAN_POINT('Ctrl Pts',(15.0291576515504,-0.00811907658734153,
3.54215900695692));
#37376=CARTESIAN_POINT('Ctrl Pts',(15.0370290236004,0.067332916148885,3.54082013248786));
#37377=CARTESIAN_POINT('Ctrl Pts',(15.0449003956503,0.143120699425059,3.55852736203643));
#37378=CARTESIAN_POINT('Ctrl Pts',(15.0527717677003,0.210167800325704,3.59316557823286));
#37379=CARTESIAN_POINT('Ctrl Pts',(15.0606431397502,0.27721490122635,3.62780379442929));
#37380=CARTESIAN_POINT('Ctrl Pts',(15.0685145118002,0.335521319751467,3.67937299727358));
#37381=CARTESIAN_POINT('Ctrl Pts',(15.0763858838501,0.378083948355844,3.74167908197646));
#37382=CARTESIAN_POINT('Ctrl Pts',(15.0842572559001,0.420646576960222,3.80398516667934));
#37383=CARTESIAN_POINT('Ctrl Pts',(15.09212862795,0.447465415643859,3.87702813324079));
#37384=CARTESIAN_POINT('Ctrl Pts',(15.1,0.455362409197302,3.95209810113337));
#37385=CARTESIAN_POINT('Ctrl Pts',(12.5,0.310062960217722,4.54266560670548));
#37386=CARTESIAN_POINT('Ctrl Pts',(12.5,0.283442099593322,4.54921865641189));
#37387=CARTESIAN_POINT('Ctrl Pts',(12.5,0.256466577744696,4.55390832200786));
#37388=CARTESIAN_POINT('Ctrl Pts',(12.5,0.229324391633413,4.55669460918752));
#37389=CARTESIAN_POINT('Ctrl Pts',(12.5,0.202804350211112,4.55941702996513));
#37390=CARTESIAN_POINT('Ctrl Pts',(12.5,0.176124140498118,4.56032157710196));
#37391=CARTESIAN_POINT('Ctrl Pts',(12.5,0.149491279718871,4.55933465732487));
#37392=CARTESIAN_POINT('Ctrl Pts',(12.5,0.131604301980395,4.55867182909064));
#37393=CARTESIAN_POINT('Ctrl Pts',(12.5,0.113739373486447,4.5571550748263));
#37394=CARTESIAN_POINT('Ctrl Pts',(12.5,0.0959711573489174,4.5547553284502));
#37395=CARTESIAN_POINT('Ctrl Pts',(12.5,0.0885102514788159,4.55374767063663));
#37396=CARTESIAN_POINT('Ctrl Pts',(12.5,0.0810658284660142,4.55258395860043));
#37397=CARTESIAN_POINT('Ctrl Pts',(12.5,0.0736590895785168,4.55126509319275));
#37398=CARTESIAN_POINT('Ctrl Pts',(12.5,0.0532014046082737,4.54762233847462));
#37399=CARTESIAN_POINT('Ctrl Pts',(12.5,0.0329999615976937,4.54279338637244));
#37400=CARTESIAN_POINT('Ctrl Pts',(12.5,0.0131662989716721,4.53674486487483));
#37401=CARTESIAN_POINT('Ctrl Pts',(12.5,-0.00550403753485725,4.53105111411095));
#37402=CARTESIAN_POINT('Ctrl Pts',(12.5,-0.0238485481480196,4.52427602479051));
#37403=CARTESIAN_POINT('Ctrl Pts',(12.5,-0.0417515783368052,4.51643454453567));
#37404=CARTESIAN_POINT('Ctrl Pts',(12.5,-0.0500477299146631,4.51280085190917));
#37405=CARTESIAN_POINT('Ctrl Pts',(12.5,-0.058248775177811,4.50893813195896));
#37406=CARTESIAN_POINT('Ctrl Pts',(12.5,-0.0663415323109863,4.50484786558969));
#37407=CARTESIAN_POINT('Ctrl Pts',(12.5,-0.0727048112135971,4.50163171746301));
#37408=CARTESIAN_POINT('Ctrl Pts',(12.5,-0.0789919703630761,4.49827952355299));
#37409=CARTESIAN_POINT('Ctrl Pts',(12.5,-0.085197598682301,4.4947927546146));
#37410=CARTESIAN_POINT('Ctrl Pts',(12.5,-0.104491803581693,4.48395188067351));
#37411=CARTESIAN_POINT('Ctrl Pts',(12.5,-0.123002674071495,4.47180959856144));
#37412=CARTESIAN_POINT('Ctrl Pts',(12.5,-0.140547257611399,4.45840101528927));
#37413=CARTESIAN_POINT('Ctrl Pts',(12.5,-0.156644205929787,4.44609879839914));
#37414=CARTESIAN_POINT('Ctrl Pts',(12.5,-0.17192740174072,4.43272977950413));
#37415=CARTESIAN_POINT('Ctrl Pts',(12.5,-0.186217277007305,4.41832740439832));
#37416=CARTESIAN_POINT('Origin',(15.1,0.,4.));
#37417=CARTESIAN_POINT('',(15.1,-1.16619037896906,2.5));
#37418=CARTESIAN_POINT('',(15.1,1.16619037896906,2.5));
#37419=CARTESIAN_POINT('',(15.1,1.25,2.5));
#37420=CARTESIAN_POINT('Origin',(15.1,0.,4.));
#37421=CARTESIAN_POINT('Origin',(15.1,0.,4.));
#37422=CARTESIAN_POINT('',(15.1,2.75545529808154E-17,5.725));
#37423=CARTESIAN_POINT('Origin',(15.1,0.,5.5));
#37424=CARTESIAN_POINT('',(15.1,1.5,4.225));
#37425=CARTESIAN_POINT('Origin',(15.1,1.5,4.));
#37426=CARTESIAN_POINT('',(15.1,-1.5,4.225));
#37427=CARTESIAN_POINT('Origin',(15.1,-1.5,4.));
#37428=CARTESIAN_POINT('Origin',(14.4,-1.5,4.));
#37429=CARTESIAN_POINT('',(14.5,-1.5,4.225));
#37430=CARTESIAN_POINT('Origin',(14.5,-1.5,4.));
#37431=CARTESIAN_POINT('',(14.4,-1.5,4.225));
#37432=CARTESIAN_POINT('Origin',(14.4,1.5,4.));
#37433=CARTESIAN_POINT('',(14.5,1.5,4.225));
#37434=CARTESIAN_POINT('Origin',(14.5,1.5,4.));
#37435=CARTESIAN_POINT('',(14.4,1.5,4.225));
#37436=CARTESIAN_POINT('Origin',(14.4,0.,5.5));
#37437=CARTESIAN_POINT('',(14.5,-2.75545529808154E-17,5.725));
#37438=CARTESIAN_POINT('Origin',(14.5,0.,5.5));
#37439=CARTESIAN_POINT('',(14.4,-2.75545529808154E-17,5.725));
#37440=CARTESIAN_POINT('Origin',(14.4,2.5,2.5));
#37441=CARTESIAN_POINT('',(14.5,1.16619037896906,2.5));
#37442=CARTESIAN_POINT('',(14.5,-1.16619037896906,2.5));
#37443=CARTESIAN_POINT('',(14.5,1.25,2.5));
#37444=CARTESIAN_POINT('',(14.5,1.16619037896906,2.5));
#37445=CARTESIAN_POINT('',(14.5,-1.16619037896906,2.5));
#37446=CARTESIAN_POINT('Origin',(14.5,0.,4.));
#37447=CARTESIAN_POINT('Origin',(14.5,0.,4.));
#37448=CARTESIAN_POINT('',(14.5,-1.34711147906209E-16,5.1));
#37449=CARTESIAN_POINT('Origin',(14.5,0.,4.));
#37450=CARTESIAN_POINT('Origin',(14.5,0.,4.));
#37451=CARTESIAN_POINT('Origin',(12.5,0.,4.));
#37452=CARTESIAN_POINT('Origin',(12.5,0.,4.));
#37453=CARTESIAN_POINT('',(12.5,-1.34711147906209E-16,5.1));
#37454=CARTESIAN_POINT('',(12.5,-1.34711147906209E-16,5.1));
#37455=CARTESIAN_POINT('Origin',(12.5,0.,4.));
#37456=CARTESIAN_POINT('Origin',(12.5,0.,4.));
#62823=UNCERTAINTY_MEASURE_WITH_UNIT(LENGTH_MEASURE(0.001),#62985,
'DISTANCE_ACCURACY_VALUE',
'Maximum model space distance between geometric entities at asserted c
onnectivities');
#62885=UNCERTAINTY_MEASURE_WITH_UNIT(LENGTH_MEASURE(0.001),#62985,
'DISTANCE_ACCURACY_VALUE',
'Maximum model space distance between geometric entities at asserted c
onnectivities');
#62922=(
GEOMETRIC_REPRESENTATION_CONTEXT(3)
GLOBAL_UNCERTAINTY_ASSIGNED_CONTEXT((#62823))
GLOBAL_UNIT_ASSIGNED_CONTEXT((#62985,#62987,#62988))
REPRESENTATION_CONTEXT('','3D')
);
#62984=(
GEOMETRIC_REPRESENTATION_CONTEXT(3)
GLOBAL_UNCERTAINTY_ASSIGNED_CONTEXT((#62885))
GLOBAL_UNIT_ASSIGNED_CONTEXT((#62985,#62987,#62988))
REPRESENTATION_CONTEXT('','3D')
);
#62985=(
LENGTH_UNIT()
NAMED_UNIT(*)
SI_UNIT(.CENTI.,.METRE.)
);
#62987=(
NAMED_UNIT(*)
PLANE_ANGLE_UNIT()
SI_UNIT($,.RADIAN.)
);
#62988=(
NAMED_UNIT(*)
SI_UNIT($,.STERADIAN.)
SOLID_ANGLE_UNIT()
);
#63025=SHAPE_DEFINITION_REPRESENTATION(#63136,#63385);
#63136=PRODUCT_DEFINITION_SHAPE('',$,#63484);
#63385=SHAPE_REPRESENTATION('',(#24752),#62922);
#63447=PRODUCT_DEFINITION_CONTEXT('part definition',#63743,'design');
#63484=PRODUCT_DEFINITION('Flanged lead nut','Flanged lead nut',#63582,
#63447);
#63582=PRODUCT_DEFINITION_FORMATION('',$,#63781);
#63743=APPLICATION_CONTEXT(
'Core Data for Automotive Mechanical Design Process');
#63744=PRODUCT_CONTEXT('part definition',#63743,'mechanical');
#63781=PRODUCT('Flanged lead nut','Flanged lead nut','Flanged lead nut',
(#63744));
#63913=COLOUR_RGB('Black',0.12,0.14,0.17);
#63914=FILL_AREA_STYLE_COLOUR('',#63913);
#63915=FILL_AREA_STYLE('',(#63914));
#63916=SURFACE_STYLE_FILL_AREA(#63915);
#63917=SURFACE_SIDE_STYLE('',(#63916));
#63918=SURFACE_STYLE_USAGE(.BOTH.,#63917);
#63919=PRESENTATION_STYLE_ASSIGNMENT((#63918));
ENDSEC;
END-ISO-10303-21;
